ISO-10303-21;
HEADER;
/* Generated by software containing ST-Developer
 * from STEP Tools, Inc. (www.steptools.com) 
 */

FILE_DESCRIPTION(
/* description */ ('Independent equipment support assembly with bolted 600 x 500 mm welde
d perimeter frame, four adjustable legs and swivel feet. Nominal overa
ll height 518 mm. No load rating assigned.'),
/* implementation_level */ '2;1');

FILE_NAME(
/* name */ 'Lock nut M10.step',
/* time_stamp */ '2026-11-07T17:30:39-08:00',
/* author */ (''),
/* organization */ (''),
/* preprocessor_version */ 'ST-DEVELOPER v20.2',
/* originating_system */ 'Autodesk Translation Framework v15.17.0.0',
/* authorisation */ '');

FILE_SCHEMA (('AUTOMOTIVE_DESIGN { 1 0 10303 214 3 1 1 }'));
ENDSEC;

DATA;
#10=MECHANICAL_DESIGN_GEOMETRIC_PRESENTATION_REPRESENTATION('',(#2220),#63755);
#281=B_SPLINE_SURFACE_WITH_KNOTS('',3,3,((#60172,#60173,#60174,#60175,#60176,
#60177,#60178,#60179,#60180,#60181,#60182,#60183,#60184,#60185,#60186,#60187,
#60188,#60189,#60190,#60191,#60192,#60193,#60194,#60195,#60196,#60197,#60198,
#60199,#60200,#60201,#60202,#60203,#60204,#60205,#60206,#60207,#60208,#60209,
#60210,#60211,#60212,#60213,#60214,#60215,#60216,#60217,#60218,#60219,#60220,
#60221,#60222,#60223,#60224,#60225,#60226,#60227,#60228,#60229),(#60230,
#60231,#60232,#60233,#60234,#60235,#60236,#60237,#60238,#60239,#60240,#60241,
#60242,#60243,#60244,#60245,#60246,#60247,#60248,#60249,#60250,#60251,#60252,
#60253,#60254,#60255,#60256,#60257,#60258,#60259,#60260,#60261,#60262,#60263,
#60264,#60265,#60266,#60267,#60268,#60269,#60270,#60271,#60272,#60273,#60274,
#60275,#60276,#60277,#60278,#60279,#60280,#60281,#60282,#60283,#60284,#60285,
#60286,#60287),(#60288,#60289,#60290,#60291,#60292,#60293,#60294,#60295,
#60296,#60297,#60298,#60299,#60300,#60301,#60302,#60303,#60304,#60305,#60306,
#60307,#60308,#60309,#60310,#60311,#60312,#60313,#60314,#60315,#60316,#60317,
#60318,#60319,#60320,#60321,#60322,#60323,#60324,#60325,#60326,#60327,#60328,
#60329,#60330,#60331,#60332,#60333,#60334,#60335,#60336,#60337,#60338,#60339,
#60340,#60341,#60342,#60343,#60344,#60345),(#60346,#60347,#60348,#60349,
#60350,#60351,#60352,#60353,#60354,#60355,#60356,#60357,#60358,#60359,#60360,
#60361,#60362,#60363,#60364,#60365,#60366,#60367,#60368,#60369,#60370,#60371,
#60372,#60373,#60374,#60375,#60376,#60377,#60378,#60379,#60380,#60381,#60382,
#60383,#60384,#60385,#60386,#60387,#60388,#60389,#60390,#60391,#60392,#60393,
#60394,#60395,#60396,#60397,#60398,#60399,#60400,#60401,#60402,#60403)),
 .UNSPECIFIED.,.F.,.F.,.F.,(4,4),(4,1,1,1,1,1,1,1,1,1,1,1,1,1,1,1,1,1,1,
1,1,1,1,1,1,1,1,1,1,1,1,1,1,1,1,1,1,1,1,1,1,1,1,1,1,1,1,1,1,1,1,1,1,1,1,
4),(0.,0.0641840294258107),(11.8589888623078,12.3522141756159,12.8454394889239,
13.8318901155401,14.8183407421562,15.8047913687724,16.7912419953885,17.7776926220047,
18.7641432486208,19.750593875237,20.7370445018531,21.7234951284693,22.7099457550854,
23.6963963817016,24.6828470083177,25.6692976349339,26.65574826155,27.6421988881662,
28.6286495147823,29.6151001413985,30.6015507680146,31.5880013946308,32.5744520212469,
33.5609026478631,34.5473532744792,35.5338039010954,36.5202545277115,37.5067051543277,
38.4931557809438,39.47960640756,40.4660570341761,41.4525076607923,42.4389582874084,
43.4254089140245,44.4118595406407,45.3983101672568,46.384760793873,47.3712114204891,
48.3576620471053,49.3441126737214,50.3305633003376,51.3170139269537,52.3034645535699,
53.289915180186,54.2763658068022,55.2628164334183,56.2492670600345,57.2357176866506,
58.2221683132668,59.2086189398829,60.1950695664991,61.1815201931152,62.1679708197314,
63.1544214463475,63.6476467596556,64.1408720729637),.UNSPECIFIED.);
#282=B_SPLINE_SURFACE_WITH_KNOTS('',3,3,((#60638,#60639,#60640,#60641,#60642,
#60643,#60644,#60645,#60646,#60647,#60648,#60649,#60650,#60651,#60652,#60653,
#60654,#60655,#60656,#60657,#60658,#60659,#60660,#60661,#60662,#60663,#60664,
#60665,#60666,#60667,#60668,#60669,#60670,#60671,#60672,#60673,#60674,#60675,
#60676,#60677,#60678,#60679,#60680,#60681,#60682,#60683,#60684,#60685,#60686,
#60687,#60688,#60689,#60690,#60691,#60692,#60693,#60694,#60695),(#60696,
#60697,#60698,#60699,#60700,#60701,#60702,#60703,#60704,#60705,#60706,#60707,
#60708,#60709,#60710,#60711,#60712,#60713,#60714,#60715,#60716,#60717,#60718,
#60719,#60720,#60721,#60722,#60723,#60724,#60725,#60726,#60727,#60728,#60729,
#60730,#60731,#60732,#60733,#60734,#60735,#60736,#60737,#60738,#60739,#60740,
#60741,#60742,#60743,#60744,#60745,#60746,#60747,#60748,#60749,#60750,#60751,
#60752,#60753),(#60754,#60755,#60756,#60757,#60758,#60759,#60760,#60761,
#60762,#60763,#60764,#60765,#60766,#60767,#60768,#60769,#60770,#60771,#60772,
#60773,#60774,#60775,#60776,#60777,#60778,#60779,#60780,#60781,#60782,#60783,
#60784,#60785,#60786,#60787,#60788,#60789,#60790,#60791,#60792,#60793,#60794,
#60795,#60796,#60797,#60798,#60799,#60800,#60801,#60802,#60803,#60804,#60805,
#60806,#60807,#60808,#60809,#60810,#60811),(#60812,#60813,#60814,#60815,
#60816,#60817,#60818,#60819,#60820,#60821,#60822,#60823,#60824,#60825,#60826,
#60827,#60828,#60829,#60830,#60831,#60832,#60833,#60834,#60835,#60836,#60837,
#60838,#60839,#60840,#60841,#60842,#60843,#60844,#60845,#60846,#60847,#60848,
#60849,#60850,#60851,#60852,#60853,#60854,#60855,#60856,#60857,#60858,#60859,
#60860,#60861,#60862,#60863,#60864,#60865,#60866,#60867,#60868,#60869)),
 .UNSPECIFIED.,.F.,.F.,.F.,(4,4),(4,1,1,1,1,1,1,1,1,1,1,1,1,1,1,1,1,1,1,
1,1,1,1,1,1,1,1,1,1,1,1,1,1,1,1,1,1,1,1,1,1,1,1,1,1,1,1,1,1,1,1,1,1,1,1,
4),(0.,0.0641840294258107),(14.3989442667811,14.8921695800892,15.3853948933972,
16.3718455200134,17.3582961466295,18.3447467732457,19.3311973998618,20.317648026478,
21.3040986530941,22.2905492797103,23.2769999063264,24.2634505329426,25.2499011595587,
26.2363517861749,27.222802412791,28.2092530394072,29.1957036660233,30.1821542926395,
31.1686049192556,32.1550555458718,33.1415061724879,34.1279567991041,35.1144074257202,
36.1008580523364,37.0873086789525,38.0737593055687,39.0602099321848,40.046660558801,
41.0331111854171,42.0195618120333,43.0060124386494,43.9924630652656,44.9789136918817,
45.9653643184979,46.951814945114,47.9382655717301,48.9247161983463,49.9111668249625,
50.8976174515786,51.8840680781948,52.8705187048109,53.856969331427,54.8434199580432,
55.8298705846593,56.8163212112755,57.8027718378916,58.7892224645078,59.7756730911239,
60.7621237177401,61.7485743443562,62.7350249709724,63.7214755975885,64.7079262242047,
65.6943768508208,66.1876021641289,66.680827477437),.UNSPECIFIED.);
#468=CIRCLE('',#15396,4.51775);
#469=CIRCLE('',#15404,4.51775);
#470=CIRCLE('',#15406,5.0736);
#471=CIRCLE('',#15414,5.0736);
#1481=B_SPLINE_CURVE_WITH_KNOTS('',3,(#59598,#59599,#59600,#59601,#59602,
#59603,#59604),.UNSPECIFIED.,.F.,.F.,(4,3,4),(51.5745014586045,51.7886578973478,
52.2818832106559),.UNSPECIFIED.);
#1482=B_SPLINE_CURVE_WITH_KNOTS('',3,(#59607,#59608,#59609,#59610,#59611,
#59612,#59613,#59614,#59615,#59616),.UNSPECIFIED.,.F.,.F.,(4,3,3,4),(-50.2654824574367,
-49.3225313308074,-48.3360807041913,-47.8312715558983),.UNSPECIFIED.);
#1483=B_SPLINE_CURVE_WITH_KNOTS('',3,(#59621,#59622,#59623,#59624,#59625,
#59626,#59627,#59628,#59629,#59630,#59631,#59632,#59633,#59634,#59635,#59636,
#59637,#59638,#59639,#59640,#59641,#59642,#59643,#59644,#59645),
 .UNSPECIFIED.,.F.,.F.,(4,3,3,3,3,3,3,3,4),(45.291316151425,45.3767288243428,
46.363179450959,47.3496300775751,48.3360807041913,49.3225313308074,50.3089819574236,
51.2954325840397,51.5745014586045),.UNSPECIFIED.);
#1484=B_SPLINE_CURVE_WITH_KNOTS('',3,(#59646,#59647,#59648,#59649,#59650,
#59651,#59652,#59653,#59654,#59655,#59656,#59657,#59658,#59659,#59660,#59661,
#59662,#59663,#59664,#59665,#59666,#59667),.UNSPECIFIED.,.F.,.F.,(4,3,3,
3,3,3,3,4),(-47.8312715558983,-47.3496300775751,-46.363179450959,-45.3767288243428,
-44.3902781977267,-43.4038275711106,-42.4173769444944,-41.5480862487187),
 .UNSPECIFIED.);
#1485=B_SPLINE_CURVE_WITH_KNOTS('',3,(#59672,#59673,#59674,#59675,#59676,
#59677,#59678,#59679,#59680,#59681,#59682,#59683,#59684,#59685,#59686,#59687,
#59688,#59689,#59690,#59691,#59692,#59693),.UNSPECIFIED.,.F.,.F.,(4,3,3,
3,3,3,3,4),(39.0081308442454,39.458025064646,40.4444756912621,41.4309263178782,
42.4173769444944,43.4038275711105,44.3902781977267,45.291316151425),
 .UNSPECIFIED.);
#1486=B_SPLINE_CURVE_WITH_KNOTS('',3,(#59694,#59695,#59696,#59697,#59698,
#59699,#59700,#59701,#59702,#59703,#59704,#59705,#59706,#59707,#59708,#59709,
#59710,#59711,#59712,#59713,#59714,#59715,#59716,#59717,#59718),
 .UNSPECIFIED.,.F.,.F.,(4,3,3,3,3,3,3,3,4),(-41.5480862487187,-41.4309263178783,
-40.4444756912621,-39.458025064646,-38.4715744380298,-37.4851238114137,
-36.4986731847975,-35.5122225581814,-35.2649009415391),.UNSPECIFIED.);
#1487=B_SPLINE_CURVE_WITH_KNOTS('',3,(#59723,#59724,#59725,#59726,#59727,
#59728,#59729,#59730,#59731,#59732,#59733,#59734,#59735,#59736,#59737,#59738,
#59739,#59740,#59741,#59742,#59743,#59744),.UNSPECIFIED.,.F.,.F.,(4,3,3,
3,3,3,3,4),(32.7249455370658,33.5393213049491,34.5257719315652,35.5122225581814,
36.4986731847975,37.4851238114137,38.4715744380298,39.0081308442454),
 .UNSPECIFIED.);
#1488=B_SPLINE_CURVE_WITH_KNOTS('',3,(#59745,#59746,#59747,#59748,#59749,
#59750,#59751,#59752,#59753,#59754,#59755,#59756,#59757,#59758,#59759,#59760,
#59761,#59762,#59763,#59764,#59765,#59766),.UNSPECIFIED.,.F.,.F.,(4,3,3,
3,3,3,3,4),(-35.2649009415391,-34.5257719315652,-33.5393213049491,-32.5528706783329,
-31.5664200517168,-30.5799694251006,-29.5935187984845,-28.9817156343595),
 .UNSPECIFIED.);
#1489=B_SPLINE_CURVE_WITH_KNOTS('',3,(#59771,#59772,#59773,#59774,#59775,
#59776,#59777,#59778,#59779,#59780,#59781,#59782,#59783,#59784,#59785,#59786,
#59787,#59788,#59789,#59790,#59791,#59792,#59793,#59794,#59795),
 .UNSPECIFIED.,.F.,.F.,(4,3,3,3,3,3,3,3,4),(26.4417602298862,26.634166918636,
27.6206175452522,28.6070681718683,29.5935187984845,30.5799694251006,31.5664200517168,
32.5528706783329,32.7249455370658),.UNSPECIFIED.);
#1490=B_SPLINE_CURVE_WITH_KNOTS('',3,(#59796,#59797,#59798,#59799,#59800,
#59801,#59802,#59803,#59804,#59805,#59806,#59807,#59808,#59809,#59810,#59811,
#59812,#59813,#59814,#59815,#59816,#59817),.UNSPECIFIED.,.F.,.F.,(4,3,3,
3,3,3,3,4),(-28.9817156343595,-28.6070681718683,-27.6206175452522,-26.634166918636,
-25.6477162920199,-24.6612656654037,-23.6748150387876,-22.6985303271799),
 .UNSPECIFIED.);
#1491=B_SPLINE_CURVE_WITH_KNOTS('',3,(#59822,#59823,#59824,#59825,#59826,
#59827,#59828,#59829,#59830,#59831,#59832,#59833,#59834,#59835,#59836,#59837,
#59838,#59839,#59840,#59841,#59842,#59843),.UNSPECIFIED.,.F.,.F.,(4,3,3,
3,3,3,3,4),(20.1585749227066,20.7154631589391,21.7019137855553,22.6883644121714,
23.6748150387876,24.6612656654037,25.6477162920199,26.4417602298862),
 .UNSPECIFIED.);
#1492=B_SPLINE_CURVE_WITH_KNOTS('',3,(#59844,#59845,#59846,#59847,#59848,
#59849,#59850,#59851,#59852,#59853,#59854,#59855,#59856,#59857,#59858,#59859,
#59860,#59861,#59862,#59863,#59864,#59865,#59866,#59867,#59868),
 .UNSPECIFIED.,.F.,.F.,(4,3,3,3,3,3,3,3,4),(-22.6985303271799,-22.6883644121714,
-21.7019137855553,-20.7154631589391,-19.729012532323,-18.7425619057068,
-17.7561112790907,-16.7696606524745,-16.4153450200003),.UNSPECIFIED.);
#1493=B_SPLINE_CURVE_WITH_KNOTS('',3,(#59873,#59874,#59875,#59876,#59877,
#59878,#59879,#59880,#59881,#59882,#59883,#59884,#59885,#59886,#59887,#59888,
#59889,#59890,#59891,#59892,#59893,#59894),.UNSPECIFIED.,.F.,.F.,(4,3,3,
3,3,3,3,4),(13.875389615527,14.7967593992422,15.7832100258584,16.7696606524745,
17.7561112790907,18.7425619057068,19.729012532323,20.1585749227066),
 .UNSPECIFIED.);
#1494=B_SPLINE_CURVE_WITH_KNOTS('',3,(#59895,#59896,#59897,#59898,#59899,
#59900,#59901,#59902,#59903,#59904,#59905,#59906,#59907,#59908,#59909,#59910,
#59911,#59912,#59913,#59914,#59915,#59916),.UNSPECIFIED.,.F.,.F.,(4,3,3,
3,3,3,3,4),(-16.4153450200003,-15.7832100258584,-14.7967593992422,-13.8103087726261,
-12.8238581460099,-11.8374075193938,-10.8509568927776,-10.1321597128207),
 .UNSPECIFIED.);
#1495=B_SPLINE_CURVE_WITH_KNOTS('',3,(#59922,#59923,#59924,#59925,#59926,
#59927,#59928,#59929,#59930,#59931,#59932,#59933,#59934,#59935,#59936,#59937),
 .UNSPECIFIED.,.F.,.F.,(4,3,3,3,3,4),(-3.84897440564117,-2.95935187984845,
-1.9729012532323,-0.986450626616147,-0.493225313308074,0.),
 .UNSPECIFIED.);
#1496=B_SPLINE_CURVE_WITH_KNOTS('',3,(#59940,#59941,#59942,#59943,#59944,
#59945,#59946,#59947,#59948,#59949,#59950,#59951,#59952,#59953,#59954,#59955,
#59956,#59957,#59958),.UNSPECIFIED.,.F.,.F.,(4,3,3,3,3,3,4),(2.01640075321919,
2.95935187984845,3.9458025064646,4.93225313308074,5.9187037596969,6.90515438631305,
7.59220430834742),.UNSPECIFIED.);
#1497=B_SPLINE_CURVE_WITH_KNOTS('',3,(#59964,#59965,#59966,#59967,#59968,
#59969,#59970,#59971,#59972),.UNSPECIFIED.,.F.,.F.,(4,1,1,1,1,1,4),(59.6902604182061,
60.1950695664991,61.1815201931152,62.1679708197314,63.1544214463475,63.6476467596556,
64.1408720729637),.UNSPECIFIED.);
#1498=B_SPLINE_CURVE_WITH_KNOTS('',3,(#59975,#59976,#59977,#59978,#59979,
#59980,#59981,#59982,#59983),.UNSPECIFIED.,.F.,.F.,(4,1,1,1,1,1,4),(59.6902604182061,
59.7756730911239,60.7621237177401,61.7485743443562,62.7350249709724,63.7214755975885,
64.6644267242178),.UNSPECIFIED.);
#1499=B_SPLINE_CURVE_WITH_KNOTS('',3,(#59988,#59989,#59990,#59991,#59992,
#59993,#59994,#59995,#59996,#59997),.UNSPECIFIED.,.F.,.F.,(4,1,1,1,1,1,
1,4),(53.4070751110265,54.2763658068022,55.2628164334183,56.2492670600345,
57.2357176866506,58.2221683132668,59.2086189398829,59.6902604182061),
 .UNSPECIFIED.);
#1500=B_SPLINE_CURVE_WITH_KNOTS('',3,(#59998,#59999,#60000,#60001,#60002,
#60003,#60004,#60005,#60006,#60007),.UNSPECIFIED.,.F.,.F.,(4,1,1,1,1,1,
1,4),(53.4070751110265,53.856969331427,54.8434199580432,55.8298705846593,
56.8163212112755,57.8027718378916,58.7892224645078,59.6902604182061),
 .UNSPECIFIED.);
#1501=B_SPLINE_CURVE_WITH_KNOTS('',3,(#60012,#60013,#60014,#60015,#60016,
#60017,#60018,#60019,#60020,#60021,#60022),.UNSPECIFIED.,.F.,.F.,(4,1,1,
1,1,1,1,1,4),(47.1238898038469,47.3712114204891,48.3576620471053,49.3441126737214,
50.3305633003376,51.3170139269537,52.3034645535699,53.289915180186,53.4070751110265),
 .UNSPECIFIED.);
#1502=B_SPLINE_CURVE_WITH_KNOTS('',3,(#60023,#60024,#60025,#60026,#60027,
#60028,#60029,#60030,#60031,#60032),.UNSPECIFIED.,.F.,.F.,(4,1,1,1,1,1,
1,4),(47.1238898038469,47.9382655717301,48.9247161983463,49.9111668249625,
50.8976174515786,51.8840680781948,52.8705187048109,53.4070751110265),
 .UNSPECIFIED.);
#1503=B_SPLINE_CURVE_WITH_KNOTS('',3,(#60037,#60038,#60039,#60040,#60041,
#60042,#60043,#60044,#60045,#60046),.UNSPECIFIED.,.F.,.F.,(4,1,1,1,1,1,
1,4),(40.8407044966673,41.4525076607923,42.4389582874084,43.4254089140245,
44.4118595406407,45.3983101672568,46.384760793873,47.1238898038469),
 .UNSPECIFIED.);
#1504=B_SPLINE_CURVE_WITH_KNOTS('',3,(#60047,#60048,#60049,#60050,#60051,
#60052,#60053,#60054,#60055,#60056,#60057),.UNSPECIFIED.,.F.,.F.,(4,1,1,
1,1,1,1,1,4),(40.8407044966673,41.0331111854171,42.0195618120333,43.0060124386494,
43.9924630652656,44.9789136918817,45.9653643184979,46.951814945114,47.1238898038469),
 .UNSPECIFIED.);
#1505=B_SPLINE_CURVE_WITH_KNOTS('',3,(#60062,#60063,#60064,#60065,#60066,
#60067,#60068,#60069,#60070,#60071),.UNSPECIFIED.,.F.,.F.,(4,1,1,1,1,1,
1,4),(34.5575191894877,35.5338039010954,36.5202545277115,37.5067051543277,
38.4931557809438,39.47960640756,40.4660570341761,40.8407044966673),
 .UNSPECIFIED.);
#1506=B_SPLINE_CURVE_WITH_KNOTS('',3,(#60072,#60073,#60074,#60075,#60076,
#60077,#60078,#60079,#60080,#60081),.UNSPECIFIED.,.F.,.F.,(4,1,1,1,1,1,
1,4),(34.5575191894877,35.1144074257202,36.1008580523364,37.0873086789525,
38.0737593055687,39.0602099321848,40.046660558801,40.8407044966673),
 .UNSPECIFIED.);
#1507=B_SPLINE_CURVE_WITH_KNOTS('',3,(#60086,#60087,#60088,#60089,#60090,
#60091,#60092,#60093,#60094,#60095,#60096),.UNSPECIFIED.,.F.,.F.,(4,1,1,
1,1,1,1,1,4),(28.2743338823081,28.6286495147823,29.6151001413985,30.6015507680146,
31.5880013946308,32.5744520212469,33.5609026478631,34.5473532744792,34.5575191894877),
 .UNSPECIFIED.);
#1508=B_SPLINE_CURVE_WITH_KNOTS('',3,(#60097,#60098,#60099,#60100,#60101,
#60102,#60103,#60104,#60105,#60106),.UNSPECIFIED.,.F.,.F.,(4,1,1,1,1,1,
1,4),(28.2743338823081,29.1957036660233,30.1821542926395,31.1686049192556,
32.1550555458718,33.1415061724879,34.1279567991041,34.5575191894877),
 .UNSPECIFIED.);
#1509=B_SPLINE_CURVE_WITH_KNOTS('',3,(#60111,#60112,#60113,#60114,#60115,
#60116,#60117,#60118,#60119,#60120),.UNSPECIFIED.,.F.,.F.,(4,1,1,1,1,1,
1,4),(21.9911485751285,22.7099457550854,23.6963963817016,24.6828470083177,
25.6692976349339,26.65574826155,27.6421988881662,28.2743338823081),
 .UNSPECIFIED.);
#1510=B_SPLINE_CURVE_WITH_KNOTS('',3,(#60121,#60122,#60123,#60124,#60125,
#60126,#60127,#60128,#60129,#60130,#60131),.UNSPECIFIED.,.F.,.F.,(4,1,1,
1,1,1,1,1,4),(21.9911485751285,22.2905492797103,23.2769999063264,24.2634505329426,
25.2499011595587,26.2363517861749,27.222802412791,28.2092530394072,28.2743338823081),
 .UNSPECIFIED.);
#1511=B_SPLINE_CURVE_WITH_KNOTS('',3,(#60137,#60138,#60139,#60140,#60141,
#60142),.UNSPECIFIED.,.F.,.F.,(4,1,1,4),(14.3989442667811,14.8921695800892,
15.3853948933972,15.7079632679489),.UNSPECIFIED.);
#1512=B_SPLINE_CURVE_WITH_KNOTS('',3,(#60145,#60146,#60147,#60148,#60149),
 .UNSPECIFIED.,.F.,.F.,(4,1,4),(13.875389615527,14.8183407421562,15.7079632679489),
 .UNSPECIFIED.);
#1513=B_SPLINE_CURVE_WITH_KNOTS('',3,(#60151,#60152,#60153,#60154,#60155,
#60156,#60157,#60158,#60159,#60160,#60161),.UNSPECIFIED.,.F.,.F.,(4,1,1,
1,1,1,1,1,4),(15.7079632679489,15.8047913687724,16.7912419953885,17.7776926220047,
18.7641432486208,19.750593875237,20.7370445018531,21.7234951284693,21.9911485751285),
 .UNSPECIFIED.);
#1514=B_SPLINE_CURVE_WITH_KNOTS('',3,(#60162,#60163,#60164,#60165,#60166,
#60167,#60168,#60169,#60170,#60171),.UNSPECIFIED.,.F.,.F.,(4,1,1,1,1,1,
1,4),(15.7079632679489,16.3718455200134,17.3582961466295,18.3447467732457,
19.3311973998618,20.317648026478,21.3040986530941,21.9911485751285),
 .UNSPECIFIED.);
#1515=B_SPLINE_CURVE_WITH_KNOTS('',3,(#60404,#60405,#60406,#60407,#60408,
#60409,#60410,#60411,#60412,#60413,#60414,#60415,#60416,#60417,#60418,#60419,
#60420,#60421,#60422,#60423,#60424,#60425,#60426,#60427,#60428,#60429,#60430,
#60431,#60432,#60433,#60434,#60435,#60436,#60437,#60438,#60439,#60440,#60441,
#60442,#60443,#60444,#60445,#60446,#60447,#60448,#60449,#60450,#60451,#60452,
#60453,#60454,#60455,#60456,#60457,#60458,#60459,#60460,#60461,#60462,#60463,
#60464,#60465,#60466,#60467,#60468,#60469,#60470,#60471,#60472,#60473,#60474,
#60475,#60476,#60477,#60478,#60479,#60480,#60481,#60482,#60483,#60484,#60485,
#60486,#60487,#60488,#60489,#60490,#60491,#60492,#60493,#60494,#60495,#60496,
#60497,#60498,#60499,#60500,#60501,#60502,#60503,#60504,#60505,#60506,#60507,
#60508,#60509),.UNSPECIFIED.,.F.,.F.,(4,3,3,3,3,3,3,3,3,3,3,3,3,3,3,3,3,
3,3,3,3,3,3,3,3,3,3,3,3,3,3,3,3,3,3,4),(0.,0.0439873495596682,0.088535234885729,
0.133203648537345,0.177539443303643,0.193269018030229,0.199971189808446,
0.243934275067846,0.248071778815114,0.292055723719706,0.335717872507241,
0.374210944067843,0.384315712222397,0.391619070879034,0.434698852730331,
0.47712046629841,0.48969015874965,0.533088907914198,0.559308924386188,0.574291000021554,
0.57984588764462,0.62205897872085,0.66496509314549,0.707636118884185,0.738257750456918,
0.752576412624451,0.758605909671541,0.765028679465915,0.807111218921827,
0.843485707057882,0.85917048475052,0.866049641644265,0.873236607794053,
0.913787166992983,0.952609171466047,0.972375876542335),.UNSPECIFIED.);
#1516=B_SPLINE_CURVE_WITH_KNOTS('',3,(#60510,#60511,#60512,#60513,#60514,
#60515,#60516,#60517,#60518,#60519,#60520,#60521,#60522,#60523,#60524,#60525,
#60526,#60527,#60528,#60529,#60530,#60531,#60532,#60533,#60534,#60535,#60536,
#60537,#60538,#60539,#60540,#60541,#60542,#60543,#60544,#60545,#60546,#60547,
#60548,#60549,#60550,#60551,#60552,#60553,#60554,#60555,#60556,#60557,#60558,
#60559,#60560,#60561,#60562,#60563,#60564,#60565,#60566,#60567,#60568,#60569,
#60570,#60571,#60572,#60573,#60574,#60575,#60576,#60577,#60578,#60579,#60580,
#60581,#60582,#60583,#60584,#60585,#60586,#60587,#60588,#60589,#60590,#60591,
#60592,#60593,#60594,#60595,#60596,#60597,#60598,#60599,#60600,#60601,#60602,
#60603,#60604,#60605,#60606,#60607,#60608,#60609,#60610,#60611,#60612),
 .UNSPECIFIED.,.F.,.F.,(4,3,3,3,3,3,3,3,3,3,3,3,3,3,3,3,3,3,3,3,3,3,3,3,
3,3,3,3,3,3,3,3,3,3,4),(0.,0.0403422905180338,0.0813682734786595,0.122949980351713,
0.16449095941097,0.178014361827899,0.183409369411602,0.227186329885339,
0.269229509469957,0.311535350955759,0.348916065443153,0.357705618004978,
0.364415764229672,0.407315005273426,0.450191512111689,0.461058208905336,
0.503507289353387,0.531285871131442,0.541027225498738,0.546474827271459,
0.552442453195144,0.594916660917874,0.639047653028424,0.683117962531696,
0.716223791940519,0.731747366121405,0.738184546707727,0.782779716156374,
0.824075936567849,0.84301368069624,0.852796512264844,0.860145827789084,
0.904729831180339,0.947964597802275,0.97000658757344),.UNSPECIFIED.);
#1517=B_SPLINE_CURVE_WITH_KNOTS('',3,(#60613,#60614,#60615,#60616,#60617,
#60618,#60619,#60620,#60621,#60622,#60623,#60624,#60625,#60626,#60627,#60628,
#60629,#60630,#60631,#60632,#60633,#60634,#60635,#60636,#60637),
 .UNSPECIFIED.,.F.,.F.,(4,3,3,3,3,3,3,3,4),(-10.1321597128207,-9.86450626616149,
-8.87805563954534,-7.89160501292919,-6.90515438631305,-5.91870375969689,
-4.93225313308075,-3.94580250646459,-3.84897440564117),.UNSPECIFIED.);
#1518=B_SPLINE_CURVE_WITH_KNOTS('',3,(#60870,#60871,#60872,#60873,#60874,
#60875,#60876,#60877,#60878,#60879,#60880,#60881,#60882,#60883,#60884,#60885,
#60886,#60887,#60888,#60889,#60890,#60891,#60892,#60893,#60894,#60895,#60896,
#60897,#60898,#60899,#60900,#60901,#60902,#60903,#60904,#60905,#60906,#60907,
#60908,#60909,#60910,#60911,#60912,#60913,#60914,#60915,#60916,#60917,#60918,
#60919,#60920,#60921,#60922,#60923,#60924,#60925,#60926,#60927,#60928,#60929,
#60930,#60931,#60932,#60933,#60934,#60935,#60936,#60937,#60938,#60939,#60940,
#60941,#60942,#60943,#60944,#60945,#60946,#60947,#60948,#60949,#60950,#60951,
#60952,#60953,#60954,#60955,#60956,#60957,#60958,#60959,#60960,#60961,#60962,
#60963,#60964,#60965,#60966,#60967,#60968,#60969,#60970,#60971,#60972),
 .UNSPECIFIED.,.F.,.F.,(4,3,3,3,3,3,3,3,3,3,3,3,3,3,3,3,3,3,3,3,3,3,3,3,
3,3,3,3,3,3,3,3,3,3,4),(0.,0.0403420728543006,0.0813678367855401,0.122949539928715,
0.164490759249614,0.178014431809021,0.183409385478703,0.227186329885338,
0.269229949539637,0.311536068831159,0.348916603849705,0.357706091108837,
0.364415856383174,0.407315466341614,0.450192046682075,0.461058208905346,
0.5035070595844,0.531285655723017,0.541026743529684,0.54647402973548,0.552442268108838,
0.59491621056702,0.639047258971427,0.683117463220518,0.716223355043237,
0.731746708435023,0.738183753475272,0.782778798969233,0.824075248677492,
0.843013807341498,0.852796973522259,0.860145921094186,0.904729940902664,
0.947964597802271,0.970006587573432),.UNSPECIFIED.);
#1519=B_SPLINE_CURVE_WITH_KNOTS('',3,(#60973,#60974,#60975,#60976,#60977,
#60978,#60979,#60980,#60981,#60982,#60983,#60984,#60985,#60986,#60987,#60988,
#60989,#60990,#60991,#60992,#60993,#60994,#60995,#60996,#60997),
 .UNSPECIFIED.,.F.,.F.,(4,3,3,3,3,3,3,3,4),(7.59220430834742,7.89160501292919,
8.87805563954534,9.86450626616149,10.8509568927776,11.8374075193938,12.8238581460099,
13.8103087726261,13.875389615527),.UNSPECIFIED.);
#1520=B_SPLINE_CURVE_WITH_KNOTS('',3,(#60998,#60999,#61000,#61001,#61002,
#61003,#61004,#61005,#61006,#61007,#61008,#61009,#61010,#61011,#61012,#61013,
#61014,#61015,#61016,#61017,#61018,#61019,#61020,#61021,#61022,#61023,#61024,
#61025,#61026,#61027,#61028,#61029,#61030,#61031,#61032,#61033,#61034,#61035,
#61036,#61037,#61038,#61039,#61040,#61041,#61042,#61043,#61044,#61045,#61046,
#61047,#61048,#61049,#61050,#61051,#61052,#61053,#61054,#61055,#61056,#61057,
#61058,#61059,#61060,#61061,#61062,#61063,#61064,#61065,#61066,#61067,#61068,
#61069,#61070,#61071,#61072,#61073,#61074,#61075,#61076,#61077,#61078,#61079,
#61080,#61081,#61082,#61083,#61084,#61085,#61086,#61087,#61088,#61089,#61090,
#61091,#61092,#61093,#61094,#61095,#61096,#61097,#61098,#61099,#61100,#61101,
#61102,#61103),.UNSPECIFIED.,.F.,.F.,(4,3,3,3,3,3,3,3,3,3,3,3,3,3,3,3,3,
3,3,3,3,3,3,3,3,3,3,3,3,3,3,3,3,3,3,4),(0.,0.0439870213484189,0.0885347768590274,
0.133203573182163,0.177540067473735,0.193271868519026,0.199972102087808,
0.24393536506854,0.248071778815114,0.29205601261511,0.335718137618304,0.374211142901135,
0.3843154671772,0.391619008898289,0.434698890696845,0.477120259746675,0.489690158749629,
0.533088750991939,0.55930877727157,0.574290713387234,0.579845401630218,
0.622058272372198,0.664964305291723,0.707635330968564,0.738257061030748,
0.752575428668685,0.758604644157454,0.765028377494937,0.80711091192384,
0.843485476809388,0.85917031769407,0.86604942682694,0.87323655891021,0.913787164180478,
0.95260917146603,0.972375876542318),.UNSPECIFIED.);
#2121=CYLINDRICAL_SURFACE('',#15395,4.51775);
#2122=CYLINDRICAL_SURFACE('',#15397,4.51775);
#2123=CYLINDRICAL_SURFACE('',#15398,4.51775);
#2124=CYLINDRICAL_SURFACE('',#15399,4.51775);
#2125=CYLINDRICAL_SURFACE('',#15400,4.51775);
#2126=CYLINDRICAL_SURFACE('',#15401,4.51775);
#2127=CYLINDRICAL_SURFACE('',#15402,4.51775);
#2128=CYLINDRICAL_SURFACE('',#15403,4.51775);
#2129=CYLINDRICAL_SURFACE('',#15405,5.0736);
#2130=CYLINDRICAL_SURFACE('',#15407,5.0736);
#2131=CYLINDRICAL_SURFACE('',#15408,5.0736);
#2132=CYLINDRICAL_SURFACE('',#15409,5.0736);
#2133=CYLINDRICAL_SURFACE('',#15410,5.0736);
#2134=CYLINDRICAL_SURFACE('',#15411,5.0736);
#2135=CYLINDRICAL_SURFACE('',#15412,5.0736);
#2136=CYLINDRICAL_SURFACE('',#15413,5.0736);
#2137=CYLINDRICAL_SURFACE('',#15415,5.0736);
#2138=CYLINDRICAL_SURFACE('',#15417,4.51775);
#2188=SHAPE_REPRESENTATION_RELATIONSHIP('SRR','None',#63873,#2204);
#2204=ADVANCED_BREP_SHAPE_REPRESENTATION('',(#2236),#63751);
#2220=STYLED_ITEM('',(#63962),#2236);
#2236=MANIFOLD_SOLID_BREP('Body1',#14321);
#2295=FACE_BOUND('',#3816,.T.);
#2296=FACE_BOUND('',#3825,.T.);
#2981=FACE_OUTER_BOUND('',#3796,.T.);
#2982=FACE_OUTER_BOUND('',#3797,.T.);
#2983=FACE_OUTER_BOUND('',#3798,.T.);
#2984=FACE_OUTER_BOUND('',#3799,.T.);
#2985=FACE_OUTER_BOUND('',#3800,.T.);
#2986=FACE_OUTER_BOUND('',#3801,.T.);
#2987=FACE_OUTER_BOUND('',#3802,.T.);
#2988=FACE_OUTER_BOUND('',#3803,.T.);
#2989=FACE_OUTER_BOUND('',#3804,.T.);
#2990=FACE_OUTER_BOUND('',#3805,.T.);
#2991=FACE_OUTER_BOUND('',#3806,.T.);
#2992=FACE_OUTER_BOUND('',#3807,.T.);
#2993=FACE_OUTER_BOUND('',#3808,.T.);
#2994=FACE_OUTER_BOUND('',#3809,.T.);
#2995=FACE_OUTER_BOUND('',#3810,.T.);
#2996=FACE_OUTER_BOUND('',#3811,.T.);
#2997=FACE_OUTER_BOUND('',#3812,.T.);
#2998=FACE_OUTER_BOUND('',#3813,.T.);
#2999=FACE_OUTER_BOUND('',#3814,.T.);
#3000=FACE_OUTER_BOUND('',#3815,.T.);
#3001=FACE_OUTER_BOUND('',#3817,.T.);
#3002=FACE_OUTER_BOUND('',#3818,.T.);
#3003=FACE_OUTER_BOUND('',#3819,.T.);
#3004=FACE_OUTER_BOUND('',#3820,.T.);
#3005=FACE_OUTER_BOUND('',#3821,.T.);
#3006=FACE_OUTER_BOUND('',#3822,.T.);
#3007=FACE_OUTER_BOUND('',#3823,.T.);
#3008=FACE_OUTER_BOUND('',#3824,.T.);
#3796=EDGE_LOOP('',(#12977,#12978,#12979,#12980));
#3797=EDGE_LOOP('',(#12981,#12982,#12983,#12984));
#3798=EDGE_LOOP('',(#12985,#12986,#12987,#12988));
#3799=EDGE_LOOP('',(#12989,#12990,#12991,#12992));
#3800=EDGE_LOOP('',(#12993,#12994,#12995,#12996));
#3801=EDGE_LOOP('',(#12997,#12998,#12999,#13000));
#3802=EDGE_LOOP('',(#13001,#13002,#13003,#13004));
#3803=EDGE_LOOP('',(#13005,#13006,#13007,#13008));
#3804=EDGE_LOOP('',(#13009,#13010,#13011,#13012));
#3805=EDGE_LOOP('',(#13013,#13014,#13015,#13016));
#3806=EDGE_LOOP('',(#13017,#13018,#13019,#13020));
#3807=EDGE_LOOP('',(#13021,#13022,#13023,#13024));
#3808=EDGE_LOOP('',(#13025,#13026,#13027,#13028));
#3809=EDGE_LOOP('',(#13029,#13030,#13031,#13032));
#3810=EDGE_LOOP('',(#13033,#13034,#13035,#13036));
#3811=EDGE_LOOP('',(#13037,#13038,#13039,#13040));
#3812=EDGE_LOOP('',(#13041,#13042,#13043,#13044));
#3813=EDGE_LOOP('',(#13045,#13046,#13047,#13048,#13049,#13050,#13051,#13052,
#13053,#13054,#13055,#13056,#13057,#13058,#13059,#13060,#13061,#13062,#13063,
#13064));
#3814=EDGE_LOOP('',(#13065,#13066,#13067,#13068,#13069,#13070,#13071,#13072,
#13073,#13074,#13075,#13076,#13077,#13078,#13079,#13080,#13081,#13082,#13083,
#13084));
#3815=EDGE_LOOP('',(#13085,#13086,#13087,#13088,#13089,#13090));
#3816=EDGE_LOOP('',(#13091,#13092,#13093,#13094));
#3817=EDGE_LOOP('',(#13095,#13096,#13097,#13098));
#3818=EDGE_LOOP('',(#13099,#13100,#13101,#13102));
#3819=EDGE_LOOP('',(#13103,#13104,#13105,#13106));
#3820=EDGE_LOOP('',(#13107,#13108,#13109,#13110));
#3821=EDGE_LOOP('',(#13111,#13112,#13113,#13114));
#3822=EDGE_LOOP('',(#13115,#13116,#13117,#13118));
#3823=EDGE_LOOP('',(#13119,#13120,#13121,#13122));
#3824=EDGE_LOOP('',(#13123,#13124,#13125,#13126,#13127,#13128));
#3825=EDGE_LOOP('',(#13129,#13130,#13131,#13132));
#4634=LINE('',#59596,#5470);
#4635=LINE('',#59620,#5471);
#4636=LINE('',#59671,#5472);
#4637=LINE('',#59722,#5473);
#4638=LINE('',#59770,#5474);
#4639=LINE('',#59821,#5475);
#4640=LINE('',#59872,#5476);
#4641=LINE('',#59920,#5477);
#4642=LINE('',#59962,#5478);
#4643=LINE('',#59987,#5479);
#4644=LINE('',#60011,#5480);
#4645=LINE('',#60036,#5481);
#4646=LINE('',#60061,#5482);
#4647=LINE('',#60085,#5483);
#4648=LINE('',#60110,#5484);
#4649=LINE('',#60135,#5485);
#4650=LINE('',#61107,#5486);
#4651=LINE('',#61109,#5487);
#4652=LINE('',#61111,#5488);
#4653=LINE('',#61113,#5489);
#4654=LINE('',#61115,#5490);
#4655=LINE('',#61116,#5491);
#4656=LINE('',#61121,#5492);
#4657=LINE('',#61122,#5493);
#4658=LINE('',#61123,#5494);
#4659=LINE('',#61126,#5495);
#4660=LINE('',#61127,#5496);
#4661=LINE('',#61130,#5497);
#4662=LINE('',#61131,#5498);
#4663=LINE('',#61134,#5499);
#4664=LINE('',#61135,#5500);
#4665=LINE('',#61138,#5501);
#4666=LINE('',#61139,#5502);
#4667=LINE('',#61141,#5503);
#5470=VECTOR('',#18051,5.);
#5471=VECTOR('',#18056,5.);
#5472=VECTOR('',#18059,5.);
#5473=VECTOR('',#18062,5.);
#5474=VECTOR('',#18065,5.);
#5475=VECTOR('',#18068,5.);
#5476=VECTOR('',#18071,5.);
#5477=VECTOR('',#18074,5.);
#5478=VECTOR('',#18079,5.0736);
#5479=VECTOR('',#18084,5.0736);
#5480=VECTOR('',#18087,5.0736);
#5481=VECTOR('',#18090,5.0736);
#5482=VECTOR('',#18093,5.0736);
#5483=VECTOR('',#18096,5.0736);
#5484=VECTOR('',#18099,5.0736);
#5485=VECTOR('',#18102,5.0736);
#5486=VECTOR('',#18109,10.);
#5487=VECTOR('',#18110,10.);
#5488=VECTOR('',#18111,10.);
#5489=VECTOR('',#18112,10.);
#5490=VECTOR('',#18113,10.);
#5491=VECTOR('',#18114,10.);
#5492=VECTOR('',#18119,10.);
#5493=VECTOR('',#18120,10.);
#5494=VECTOR('',#18121,10.);
#5495=VECTOR('',#18124,10.);
#5496=VECTOR('',#18125,10.);
#5497=VECTOR('',#18128,10.);
#5498=VECTOR('',#18129,10.);
#5499=VECTOR('',#18132,10.);
#5500=VECTOR('',#18133,10.);
#5501=VECTOR('',#18136,10.);
#5502=VECTOR('',#18137,10.);
#5503=VECTOR('',#18140,10.);
#6842=VERTEX_POINT('',#59594);
#6843=VERTEX_POINT('',#59595);
#6844=VERTEX_POINT('',#59597);
#6845=VERTEX_POINT('',#59605);
#6846=VERTEX_POINT('',#59618);
#6847=VERTEX_POINT('',#59619);
#6848=VERTEX_POINT('',#59669);
#6849=VERTEX_POINT('',#59670);
#6850=VERTEX_POINT('',#59720);
#6851=VERTEX_POINT('',#59721);
#6852=VERTEX_POINT('',#59768);
#6853=VERTEX_POINT('',#59769);
#6854=VERTEX_POINT('',#59819);
#6855=VERTEX_POINT('',#59820);
#6856=VERTEX_POINT('',#59870);
#6857=VERTEX_POINT('',#59871);
#6858=VERTEX_POINT('',#59918);
#6859=VERTEX_POINT('',#59919);
#6860=VERTEX_POINT('',#59921);
#6861=VERTEX_POINT('',#59938);
#6862=VERTEX_POINT('',#59960);
#6863=VERTEX_POINT('',#59961);
#6864=VERTEX_POINT('',#59963);
#6865=VERTEX_POINT('',#59973);
#6866=VERTEX_POINT('',#59985);
#6867=VERTEX_POINT('',#59986);
#6868=VERTEX_POINT('',#60009);
#6869=VERTEX_POINT('',#60010);
#6870=VERTEX_POINT('',#60034);
#6871=VERTEX_POINT('',#60035);
#6872=VERTEX_POINT('',#60059);
#6873=VERTEX_POINT('',#60060);
#6874=VERTEX_POINT('',#60083);
#6875=VERTEX_POINT('',#60084);
#6876=VERTEX_POINT('',#60108);
#6877=VERTEX_POINT('',#60109);
#6878=VERTEX_POINT('',#60133);
#6879=VERTEX_POINT('',#60134);
#6880=VERTEX_POINT('',#60136);
#6881=VERTEX_POINT('',#60143);
#6882=VERTEX_POINT('',#61105);
#6883=VERTEX_POINT('',#61106);
#6884=VERTEX_POINT('',#61108);
#6885=VERTEX_POINT('',#61110);
#6886=VERTEX_POINT('',#61112);
#6887=VERTEX_POINT('',#61114);
#6888=VERTEX_POINT('',#61119);
#6889=VERTEX_POINT('',#61120);
#6890=VERTEX_POINT('',#61125);
#6891=VERTEX_POINT('',#61129);
#6892=VERTEX_POINT('',#61133);
#6893=VERTEX_POINT('',#61137);
#8911=EDGE_CURVE('',#6842,#6843,#4634,.T.);
#8912=EDGE_CURVE('',#6843,#6844,#1481,.T.);
#8913=EDGE_CURVE('',#6845,#6844,#468,.F.);
#8914=EDGE_CURVE('',#6845,#6842,#1482,.T.);
#8915=EDGE_CURVE('',#6846,#6847,#4635,.T.);
#8916=EDGE_CURVE('',#6847,#6843,#1483,.T.);
#8917=EDGE_CURVE('',#6842,#6846,#1484,.T.);
#8918=EDGE_CURVE('',#6848,#6849,#4636,.T.);
#8919=EDGE_CURVE('',#6849,#6847,#1485,.T.);
#8920=EDGE_CURVE('',#6846,#6848,#1486,.T.);
#8921=EDGE_CURVE('',#6850,#6851,#4637,.T.);
#8922=EDGE_CURVE('',#6851,#6849,#1487,.T.);
#8923=EDGE_CURVE('',#6848,#6850,#1488,.T.);
#8924=EDGE_CURVE('',#6852,#6853,#4638,.T.);
#8925=EDGE_CURVE('',#6853,#6851,#1489,.T.);
#8926=EDGE_CURVE('',#6850,#6852,#1490,.T.);
#8927=EDGE_CURVE('',#6854,#6855,#4639,.T.);
#8928=EDGE_CURVE('',#6855,#6853,#1491,.T.);
#8929=EDGE_CURVE('',#6852,#6854,#1492,.T.);
#8930=EDGE_CURVE('',#6856,#6857,#4640,.T.);
#8931=EDGE_CURVE('',#6857,#6855,#1493,.T.);
#8932=EDGE_CURVE('',#6854,#6856,#1494,.T.);
#8933=EDGE_CURVE('',#6858,#6859,#4641,.T.);
#8934=EDGE_CURVE('',#6858,#6860,#1495,.T.);
#8935=EDGE_CURVE('',#6861,#6860,#469,.T.);
#8936=EDGE_CURVE('',#6861,#6859,#1496,.T.);
#8937=EDGE_CURVE('',#6862,#6863,#4642,.T.);
#8938=EDGE_CURVE('',#6863,#6864,#1497,.T.);
#8939=EDGE_CURVE('',#6865,#6864,#470,.T.);
#8940=EDGE_CURVE('',#6862,#6865,#1498,.T.);
#8941=EDGE_CURVE('',#6866,#6867,#4643,.T.);
#8942=EDGE_CURVE('',#6867,#6863,#1499,.T.);
#8943=EDGE_CURVE('',#6866,#6862,#1500,.T.);
#8944=EDGE_CURVE('',#6868,#6869,#4644,.T.);
#8945=EDGE_CURVE('',#6869,#6867,#1501,.T.);
#8946=EDGE_CURVE('',#6868,#6866,#1502,.T.);
#8947=EDGE_CURVE('',#6870,#6871,#4645,.T.);
#8948=EDGE_CURVE('',#6871,#6869,#1503,.T.);
#8949=EDGE_CURVE('',#6870,#6868,#1504,.T.);
#8950=EDGE_CURVE('',#6872,#6873,#4646,.T.);
#8951=EDGE_CURVE('',#6873,#6871,#1505,.T.);
#8952=EDGE_CURVE('',#6872,#6870,#1506,.T.);
#8953=EDGE_CURVE('',#6874,#6875,#4647,.T.);
#8954=EDGE_CURVE('',#6875,#6873,#1507,.T.);
#8955=EDGE_CURVE('',#6874,#6872,#1508,.T.);
#8956=EDGE_CURVE('',#6876,#6877,#4648,.T.);
#8957=EDGE_CURVE('',#6877,#6875,#1509,.T.);
#8958=EDGE_CURVE('',#6876,#6874,#1510,.T.);
#8959=EDGE_CURVE('',#6878,#6879,#4649,.T.);
#8960=EDGE_CURVE('',#6880,#6878,#1511,.T.);
#8961=EDGE_CURVE('',#6881,#6880,#471,.T.);
#8962=EDGE_CURVE('',#6881,#6879,#1512,.T.);
#8963=EDGE_CURVE('',#6879,#6877,#1513,.T.);
#8964=EDGE_CURVE('',#6878,#6876,#1514,.T.);
#8965=EDGE_CURVE('',#6864,#6845,#1515,.T.);
#8966=EDGE_CURVE('',#6860,#6881,#1516,.T.);
#8967=EDGE_CURVE('',#6856,#6858,#1517,.T.);
#8968=EDGE_CURVE('',#6844,#6865,#1518,.T.);
#8969=EDGE_CURVE('',#6859,#6857,#1519,.T.);
#8970=EDGE_CURVE('',#6880,#6861,#1520,.T.);
#8971=EDGE_CURVE('',#6882,#6883,#4650,.T.);
#8972=EDGE_CURVE('',#6883,#6884,#4651,.T.);
#8973=EDGE_CURVE('',#6884,#6885,#4652,.T.);
#8974=EDGE_CURVE('',#6885,#6886,#4653,.T.);
#8975=EDGE_CURVE('',#6886,#6887,#4654,.T.);
#8976=EDGE_CURVE('',#6887,#6882,#4655,.T.);
#8977=EDGE_CURVE('',#6888,#6889,#4656,.T.);
#8978=EDGE_CURVE('',#6889,#6882,#4657,.T.);
#8979=EDGE_CURVE('',#6888,#6887,#4658,.T.);
#8980=EDGE_CURVE('',#6890,#6888,#4659,.T.);
#8981=EDGE_CURVE('',#6890,#6886,#4660,.T.);
#8982=EDGE_CURVE('',#6891,#6890,#4661,.T.);
#8983=EDGE_CURVE('',#6891,#6885,#4662,.T.);
#8984=EDGE_CURVE('',#6892,#6891,#4663,.T.);
#8985=EDGE_CURVE('',#6892,#6884,#4664,.T.);
#8986=EDGE_CURVE('',#6893,#6892,#4665,.T.);
#8987=EDGE_CURVE('',#6893,#6883,#4666,.T.);
#8988=EDGE_CURVE('',#6889,#6893,#4667,.T.);
#12977=ORIENTED_EDGE('',*,*,#8911,.T.);
#12978=ORIENTED_EDGE('',*,*,#8912,.T.);
#12979=ORIENTED_EDGE('',*,*,#8913,.F.);
#12980=ORIENTED_EDGE('',*,*,#8914,.T.);
#12981=ORIENTED_EDGE('',*,*,#8915,.T.);
#12982=ORIENTED_EDGE('',*,*,#8916,.T.);
#12983=ORIENTED_EDGE('',*,*,#8911,.F.);
#12984=ORIENTED_EDGE('',*,*,#8917,.T.);
#12985=ORIENTED_EDGE('',*,*,#8918,.T.);
#12986=ORIENTED_EDGE('',*,*,#8919,.T.);
#12987=ORIENTED_EDGE('',*,*,#8915,.F.);
#12988=ORIENTED_EDGE('',*,*,#8920,.T.);
#12989=ORIENTED_EDGE('',*,*,#8921,.T.);
#12990=ORIENTED_EDGE('',*,*,#8922,.T.);
#12991=ORIENTED_EDGE('',*,*,#8918,.F.);
#12992=ORIENTED_EDGE('',*,*,#8923,.T.);
#12993=ORIENTED_EDGE('',*,*,#8924,.T.);
#12994=ORIENTED_EDGE('',*,*,#8925,.T.);
#12995=ORIENTED_EDGE('',*,*,#8921,.F.);
#12996=ORIENTED_EDGE('',*,*,#8926,.T.);
#12997=ORIENTED_EDGE('',*,*,#8927,.T.);
#12998=ORIENTED_EDGE('',*,*,#8928,.T.);
#12999=ORIENTED_EDGE('',*,*,#8924,.F.);
#13000=ORIENTED_EDGE('',*,*,#8929,.T.);
#13001=ORIENTED_EDGE('',*,*,#8930,.T.);
#13002=ORIENTED_EDGE('',*,*,#8931,.T.);
#13003=ORIENTED_EDGE('',*,*,#8927,.F.);
#13004=ORIENTED_EDGE('',*,*,#8932,.T.);
#13005=ORIENTED_EDGE('',*,*,#8933,.F.);
#13006=ORIENTED_EDGE('',*,*,#8934,.T.);
#13007=ORIENTED_EDGE('',*,*,#8935,.F.);
#13008=ORIENTED_EDGE('',*,*,#8936,.T.);
#13009=ORIENTED_EDGE('',*,*,#8937,.T.);
#13010=ORIENTED_EDGE('',*,*,#8938,.T.);
#13011=ORIENTED_EDGE('',*,*,#8939,.F.);
#13012=ORIENTED_EDGE('',*,*,#8940,.F.);
#13013=ORIENTED_EDGE('',*,*,#8941,.T.);
#13014=ORIENTED_EDGE('',*,*,#8942,.T.);
#13015=ORIENTED_EDGE('',*,*,#8937,.F.);
#13016=ORIENTED_EDGE('',*,*,#8943,.F.);
#13017=ORIENTED_EDGE('',*,*,#8944,.T.);
#13018=ORIENTED_EDGE('',*,*,#8945,.T.);
#13019=ORIENTED_EDGE('',*,*,#8941,.F.);
#13020=ORIENTED_EDGE('',*,*,#8946,.F.);
#13021=ORIENTED_EDGE('',*,*,#8947,.T.);
#13022=ORIENTED_EDGE('',*,*,#8948,.T.);
#13023=ORIENTED_EDGE('',*,*,#8944,.F.);
#13024=ORIENTED_EDGE('',*,*,#8949,.F.);
#13025=ORIENTED_EDGE('',*,*,#8950,.T.);
#13026=ORIENTED_EDGE('',*,*,#8951,.T.);
#13027=ORIENTED_EDGE('',*,*,#8947,.F.);
#13028=ORIENTED_EDGE('',*,*,#8952,.F.);
#13029=ORIENTED_EDGE('',*,*,#8953,.T.);
#13030=ORIENTED_EDGE('',*,*,#8954,.T.);
#13031=ORIENTED_EDGE('',*,*,#8950,.F.);
#13032=ORIENTED_EDGE('',*,*,#8955,.F.);
#13033=ORIENTED_EDGE('',*,*,#8956,.T.);
#13034=ORIENTED_EDGE('',*,*,#8957,.T.);
#13035=ORIENTED_EDGE('',*,*,#8953,.F.);
#13036=ORIENTED_EDGE('',*,*,#8958,.F.);
#13037=ORIENTED_EDGE('',*,*,#8959,.F.);
#13038=ORIENTED_EDGE('',*,*,#8960,.F.);
#13039=ORIENTED_EDGE('',*,*,#8961,.F.);
#13040=ORIENTED_EDGE('',*,*,#8962,.T.);
#13041=ORIENTED_EDGE('',*,*,#8959,.T.);
#13042=ORIENTED_EDGE('',*,*,#8963,.T.);
#13043=ORIENTED_EDGE('',*,*,#8956,.F.);
#13044=ORIENTED_EDGE('',*,*,#8964,.F.);
#13045=ORIENTED_EDGE('',*,*,#8965,.F.);
#13046=ORIENTED_EDGE('',*,*,#8938,.F.);
#13047=ORIENTED_EDGE('',*,*,#8942,.F.);
#13048=ORIENTED_EDGE('',*,*,#8945,.F.);
#13049=ORIENTED_EDGE('',*,*,#8948,.F.);
#13050=ORIENTED_EDGE('',*,*,#8951,.F.);
#13051=ORIENTED_EDGE('',*,*,#8954,.F.);
#13052=ORIENTED_EDGE('',*,*,#8957,.F.);
#13053=ORIENTED_EDGE('',*,*,#8963,.F.);
#13054=ORIENTED_EDGE('',*,*,#8962,.F.);
#13055=ORIENTED_EDGE('',*,*,#8966,.F.);
#13056=ORIENTED_EDGE('',*,*,#8934,.F.);
#13057=ORIENTED_EDGE('',*,*,#8967,.F.);
#13058=ORIENTED_EDGE('',*,*,#8932,.F.);
#13059=ORIENTED_EDGE('',*,*,#8929,.F.);
#13060=ORIENTED_EDGE('',*,*,#8926,.F.);
#13061=ORIENTED_EDGE('',*,*,#8923,.F.);
#13062=ORIENTED_EDGE('',*,*,#8920,.F.);
#13063=ORIENTED_EDGE('',*,*,#8917,.F.);
#13064=ORIENTED_EDGE('',*,*,#8914,.F.);
#13065=ORIENTED_EDGE('',*,*,#8968,.F.);
#13066=ORIENTED_EDGE('',*,*,#8912,.F.);
#13067=ORIENTED_EDGE('',*,*,#8916,.F.);
#13068=ORIENTED_EDGE('',*,*,#8919,.F.);
#13069=ORIENTED_EDGE('',*,*,#8922,.F.);
#13070=ORIENTED_EDGE('',*,*,#8925,.F.);
#13071=ORIENTED_EDGE('',*,*,#8928,.F.);
#13072=ORIENTED_EDGE('',*,*,#8931,.F.);
#13073=ORIENTED_EDGE('',*,*,#8969,.F.);
#13074=ORIENTED_EDGE('',*,*,#8936,.F.);
#13075=ORIENTED_EDGE('',*,*,#8970,.F.);
#13076=ORIENTED_EDGE('',*,*,#8960,.T.);
#13077=ORIENTED_EDGE('',*,*,#8964,.T.);
#13078=ORIENTED_EDGE('',*,*,#8958,.T.);
#13079=ORIENTED_EDGE('',*,*,#8955,.T.);
#13080=ORIENTED_EDGE('',*,*,#8952,.T.);
#13081=ORIENTED_EDGE('',*,*,#8949,.T.);
#13082=ORIENTED_EDGE('',*,*,#8946,.T.);
#13083=ORIENTED_EDGE('',*,*,#8943,.T.);
#13084=ORIENTED_EDGE('',*,*,#8940,.T.);
#13085=ORIENTED_EDGE('',*,*,#8971,.T.);
#13086=ORIENTED_EDGE('',*,*,#8972,.T.);
#13087=ORIENTED_EDGE('',*,*,#8973,.T.);
#13088=ORIENTED_EDGE('',*,*,#8974,.T.);
#13089=ORIENTED_EDGE('',*,*,#8975,.T.);
#13090=ORIENTED_EDGE('',*,*,#8976,.T.);
#13091=ORIENTED_EDGE('',*,*,#8966,.T.);
#13092=ORIENTED_EDGE('',*,*,#8961,.T.);
#13093=ORIENTED_EDGE('',*,*,#8970,.T.);
#13094=ORIENTED_EDGE('',*,*,#8935,.T.);
#13095=ORIENTED_EDGE('',*,*,#8933,.T.);
#13096=ORIENTED_EDGE('',*,*,#8969,.T.);
#13097=ORIENTED_EDGE('',*,*,#8930,.F.);
#13098=ORIENTED_EDGE('',*,*,#8967,.T.);
#13099=ORIENTED_EDGE('',*,*,#8977,.T.);
#13100=ORIENTED_EDGE('',*,*,#8978,.T.);
#13101=ORIENTED_EDGE('',*,*,#8976,.F.);
#13102=ORIENTED_EDGE('',*,*,#8979,.F.);
#13103=ORIENTED_EDGE('',*,*,#8980,.T.);
#13104=ORIENTED_EDGE('',*,*,#8979,.T.);
#13105=ORIENTED_EDGE('',*,*,#8975,.F.);
#13106=ORIENTED_EDGE('',*,*,#8981,.F.);
#13107=ORIENTED_EDGE('',*,*,#8982,.T.);
#13108=ORIENTED_EDGE('',*,*,#8981,.T.);
#13109=ORIENTED_EDGE('',*,*,#8974,.F.);
#13110=ORIENTED_EDGE('',*,*,#8983,.F.);
#13111=ORIENTED_EDGE('',*,*,#8984,.T.);
#13112=ORIENTED_EDGE('',*,*,#8983,.T.);
#13113=ORIENTED_EDGE('',*,*,#8973,.F.);
#13114=ORIENTED_EDGE('',*,*,#8985,.F.);
#13115=ORIENTED_EDGE('',*,*,#8986,.T.);
#13116=ORIENTED_EDGE('',*,*,#8985,.T.);
#13117=ORIENTED_EDGE('',*,*,#8972,.F.);
#13118=ORIENTED_EDGE('',*,*,#8987,.F.);
#13119=ORIENTED_EDGE('',*,*,#8988,.T.);
#13120=ORIENTED_EDGE('',*,*,#8987,.T.);
#13121=ORIENTED_EDGE('',*,*,#8971,.F.);
#13122=ORIENTED_EDGE('',*,*,#8978,.F.);
#13123=ORIENTED_EDGE('',*,*,#8988,.F.);
#13124=ORIENTED_EDGE('',*,*,#8977,.F.);
#13125=ORIENTED_EDGE('',*,*,#8980,.F.);
#13126=ORIENTED_EDGE('',*,*,#8982,.F.);
#13127=ORIENTED_EDGE('',*,*,#8984,.F.);
#13128=ORIENTED_EDGE('',*,*,#8986,.F.);
#13129=ORIENTED_EDGE('',*,*,#8965,.T.);
#13130=ORIENTED_EDGE('',*,*,#8913,.T.);
#13131=ORIENTED_EDGE('',*,*,#8968,.T.);
#13132=ORIENTED_EDGE('',*,*,#8939,.T.);
#13527=PLANE('',#15416);
#13528=PLANE('',#15418);
#13529=PLANE('',#15419);
#13530=PLANE('',#15420);
#13531=PLANE('',#15421);
#13532=PLANE('',#15422);
#13533=PLANE('',#15423);
#13534=PLANE('',#15424);
#14227=ADVANCED_FACE('',(#2981),#2121,.F.);
#14228=ADVANCED_FACE('',(#2982),#2122,.F.);
#14229=ADVANCED_FACE('',(#2983),#2123,.F.);
#14230=ADVANCED_FACE('',(#2984),#2124,.F.);
#14231=ADVANCED_FACE('',(#2985),#2125,.F.);
#14232=ADVANCED_FACE('',(#2986),#2126,.F.);
#14233=ADVANCED_FACE('',(#2987),#2127,.F.);
#14234=ADVANCED_FACE('',(#2988),#2128,.F.);
#14235=ADVANCED_FACE('',(#2989),#2129,.F.);
#14236=ADVANCED_FACE('',(#2990),#2130,.F.);
#14237=ADVANCED_FACE('',(#2991),#2131,.F.);
#14238=ADVANCED_FACE('',(#2992),#2132,.F.);
#14239=ADVANCED_FACE('',(#2993),#2133,.F.);
#14240=ADVANCED_FACE('',(#2994),#2134,.F.);
#14241=ADVANCED_FACE('',(#2995),#2135,.F.);
#14242=ADVANCED_FACE('',(#2996),#2136,.F.);
#14243=ADVANCED_FACE('',(#2997),#2137,.F.);
#14244=ADVANCED_FACE('',(#2998),#281,.F.);
#14245=ADVANCED_FACE('',(#2999),#282,.F.);
#14246=ADVANCED_FACE('',(#3000,#2295),#13527,.T.);
#14247=ADVANCED_FACE('',(#3001),#2138,.F.);
#14248=ADVANCED_FACE('',(#3002),#13528,.T.);
#14249=ADVANCED_FACE('',(#3003),#13529,.T.);
#14250=ADVANCED_FACE('',(#3004),#13530,.T.);
#14251=ADVANCED_FACE('',(#3005),#13531,.T.);
#14252=ADVANCED_FACE('',(#3006),#13532,.T.);
#14253=ADVANCED_FACE('',(#3007),#13533,.T.);
#14254=ADVANCED_FACE('',(#3008,#2296),#13534,.F.);
#14321=CLOSED_SHELL('',(#14227,#14228,#14229,#14230,#14231,#14232,#14233,
#14234,#14235,#14236,#14237,#14238,#14239,#14240,#14241,#14242,#14243,#14244,
#14245,#14246,#14247,#14248,#14249,#14250,#14251,#14252,#14253,#14254));
#15394=AXIS2_PLACEMENT_3D('',#59592,#18047,#18048);
#15395=AXIS2_PLACEMENT_3D('',#59593,#18049,#18050);
#15396=AXIS2_PLACEMENT_3D('',#59606,#18052,#18053);
#15397=AXIS2_PLACEMENT_3D('',#59617,#18054,#18055);
#15398=AXIS2_PLACEMENT_3D('',#59668,#18057,#18058);
#15399=AXIS2_PLACEMENT_3D('',#59719,#18060,#18061);
#15400=AXIS2_PLACEMENT_3D('',#59767,#18063,#18064);
#15401=AXIS2_PLACEMENT_3D('',#59818,#18066,#18067);
#15402=AXIS2_PLACEMENT_3D('',#59869,#18069,#18070);
#15403=AXIS2_PLACEMENT_3D('',#59917,#18072,#18073);
#15404=AXIS2_PLACEMENT_3D('',#59939,#18075,#18076);
#15405=AXIS2_PLACEMENT_3D('',#59959,#18077,#18078);
#15406=AXIS2_PLACEMENT_3D('',#59974,#18080,#18081);
#15407=AXIS2_PLACEMENT_3D('',#59984,#18082,#18083);
#15408=AXIS2_PLACEMENT_3D('',#60008,#18085,#18086);
#15409=AXIS2_PLACEMENT_3D('',#60033,#18088,#18089);
#15410=AXIS2_PLACEMENT_3D('',#60058,#18091,#18092);
#15411=AXIS2_PLACEMENT_3D('',#60082,#18094,#18095);
#15412=AXIS2_PLACEMENT_3D('',#60107,#18097,#18098);
#15413=AXIS2_PLACEMENT_3D('',#60132,#18100,#18101);
#15414=AXIS2_PLACEMENT_3D('',#60144,#18103,#18104);
#15415=AXIS2_PLACEMENT_3D('',#60150,#18105,#18106);
#15416=AXIS2_PLACEMENT_3D('',#61104,#18107,#18108);
#15417=AXIS2_PLACEMENT_3D('',#61117,#18115,#18116);
#15418=AXIS2_PLACEMENT_3D('',#61118,#18117,#18118);
#15419=AXIS2_PLACEMENT_3D('',#61124,#18122,#18123);
#15420=AXIS2_PLACEMENT_3D('',#61128,#18126,#18127);
#15421=AXIS2_PLACEMENT_3D('',#61132,#18130,#18131);
#15422=AXIS2_PLACEMENT_3D('',#61136,#18134,#18135);
#15423=AXIS2_PLACEMENT_3D('',#61140,#18138,#18139);
#15424=AXIS2_PLACEMENT_3D('',#61142,#18141,#18142);
#18047=DIRECTION('axis',(0.,0.,1.));
#18048=DIRECTION('refdir',(1.,0.,0.));
#18049=DIRECTION('center_axis',(0.,0.,-1.));
#18050=DIRECTION('ref_axis',(-0.346147419294793,0.938180134150982,0.));
#18051=DIRECTION('',(0.,0.,-1.));
#18052=DIRECTION('center_axis',(0.,0.,-1.));
#18053=DIRECTION('ref_axis',(1.,0.,0.));
#18054=DIRECTION('center_axis',(0.,0.,-1.));
#18055=DIRECTION('ref_axis',(1.,0.,0.));
#18056=DIRECTION('',(0.,0.,-1.));
#18057=DIRECTION('center_axis',(0.,0.,-1.));
#18058=DIRECTION('ref_axis',(1.,0.,0.));
#18059=DIRECTION('',(0.,0.,-1.));
#18060=DIRECTION('center_axis',(0.,0.,-1.));
#18061=DIRECTION('ref_axis',(1.,0.,0.));
#18062=DIRECTION('',(0.,0.,-1.));
#18063=DIRECTION('center_axis',(0.,0.,-1.));
#18064=DIRECTION('ref_axis',(1.,0.,0.));
#18065=DIRECTION('',(0.,0.,-1.));
#18066=DIRECTION('center_axis',(0.,0.,-1.));
#18067=DIRECTION('ref_axis',(1.,0.,0.));
#18068=DIRECTION('',(0.,0.,-1.));
#18069=DIRECTION('center_axis',(0.,0.,-1.));
#18070=DIRECTION('ref_axis',(1.,0.,0.));
#18071=DIRECTION('',(0.,0.,-1.));
#18072=DIRECTION('center_axis',(0.,0.,-1.));
#18073=DIRECTION('ref_axis',(0.938064160696058,-0.346461585774816,0.));
#18074=DIRECTION('',(0.,0.,-1.));
#18075=DIRECTION('center_axis',(0.,0.,-1.));
#18076=DIRECTION('ref_axis',(1.,0.,0.));
#18077=DIRECTION('center_axis',(0.,0.,-1.));
#18078=DIRECTION('ref_axis',(0.793491609261867,0.608581190993456,0.));
#18079=DIRECTION('',(1.22464679914735E-16,-2.66964461005383E-30,-1.));
#18080=DIRECTION('center_axis',(0.,0.,1.));
#18081=DIRECTION('ref_axis',(1.,-2.16768378774637E-14,0.));
#18082=DIRECTION('center_axis',(0.,0.,-1.));
#18083=DIRECTION('ref_axis',(1.,-2.16768378774637E-14,0.));
#18084=DIRECTION('',(1.22464679914735E-16,-2.66964461005383E-30,-1.));
#18085=DIRECTION('center_axis',(0.,0.,-1.));
#18086=DIRECTION('ref_axis',(1.,-2.16768378774637E-14,0.));
#18087=DIRECTION('',(1.22464679914735E-16,-2.66964461005383E-30,-1.));
#18088=DIRECTION('center_axis',(0.,0.,-1.));
#18089=DIRECTION('ref_axis',(1.,-2.16768378774637E-14,0.));
#18090=DIRECTION('',(1.22464679914735E-16,-2.66964461005383E-30,-1.));
#18091=DIRECTION('center_axis',(0.,0.,-1.));
#18092=DIRECTION('ref_axis',(1.,-2.16768378774637E-14,0.));
#18093=DIRECTION('',(1.22464679914735E-16,-2.66964461005383E-30,-1.));
#18094=DIRECTION('center_axis',(0.,0.,-1.));
#18095=DIRECTION('ref_axis',(1.,-2.16768378774637E-14,0.));
#18096=DIRECTION('',(1.22464679914735E-16,-2.66964461005383E-30,-1.));
#18097=DIRECTION('center_axis',(0.,0.,-1.));
#18098=DIRECTION('ref_axis',(1.,-2.16768378774637E-14,0.));
#18099=DIRECTION('',(1.22464679914735E-16,-2.66964461005383E-30,-1.));
#18100=DIRECTION('center_axis',(0.,0.,-1.));
#18101=DIRECTION('ref_axis',(-0.608751959302999,-0.793360606562211,0.));
#18102=DIRECTION('',(1.22464679914735E-16,-2.66964461005383E-30,-1.));
#18103=DIRECTION('center_axis',(0.,0.,-1.));
#18104=DIRECTION('ref_axis',(1.,-2.16768378774637E-14,0.));
#18105=DIRECTION('center_axis',(0.,0.,-1.));
#18106=DIRECTION('ref_axis',(1.,-2.16768378774637E-14,0.));
#18107=DIRECTION('center_axis',(0.,0.,1.));
#18108=DIRECTION('ref_axis',(1.,0.,0.));
#18109=DIRECTION('',(0.5,0.866025403784439,0.));
#18110=DIRECTION('',(-0.5,0.866025403784439,0.));
#18111=DIRECTION('',(-1.,0.,0.));
#18112=DIRECTION('',(-0.5,-0.866025403784439,0.));
#18113=DIRECTION('',(0.5,-0.866025403784439,0.));
#18114=DIRECTION('',(1.,-3.39346356420629E-16,0.));
#18115=DIRECTION('center_axis',(0.,0.,-1.));
#18116=DIRECTION('ref_axis',(1.,0.,0.));
#18117=DIRECTION('center_axis',(-3.39346356420629E-16,-1.,0.));
#18118=DIRECTION('ref_axis',(1.,-3.39346356420629E-16,0.));
#18119=DIRECTION('',(1.,-3.39346356420629E-16,0.));
#18120=DIRECTION('',(0.,0.,1.));
#18121=DIRECTION('',(0.,0.,1.));
#18122=DIRECTION('center_axis',(-0.866025403784439,-0.5,0.));
#18123=DIRECTION('ref_axis',(0.5,-0.866025403784439,0.));
#18124=DIRECTION('',(0.5,-0.866025403784439,0.));
#18125=DIRECTION('',(0.,0.,1.));
#18126=DIRECTION('center_axis',(-0.866025403784439,0.5,0.));
#18127=DIRECTION('ref_axis',(-0.5,-0.866025403784438,0.));
#18128=DIRECTION('',(-0.5,-0.866025403784439,0.));
#18129=DIRECTION('',(0.,0.,1.));
#18130=DIRECTION('center_axis',(0.,1.,0.));
#18131=DIRECTION('ref_axis',(-1.,0.,0.));
#18132=DIRECTION('',(-1.,0.,0.));
#18133=DIRECTION('',(0.,0.,1.));
#18134=DIRECTION('center_axis',(0.866025403784439,0.5,0.));
#18135=DIRECTION('ref_axis',(-0.5,0.866025403784439,0.));
#18136=DIRECTION('',(-0.5,0.866025403784439,0.));
#18137=DIRECTION('',(0.,0.,1.));
#18138=DIRECTION('center_axis',(0.866025403784439,-0.5,0.));
#18139=DIRECTION('ref_axis',(0.5,0.866025403784439,0.));
#18140=DIRECTION('',(0.5,0.866025403784439,0.));
#18141=DIRECTION('center_axis',(0.,0.,1.));
#18142=DIRECTION('ref_axis',(1.,0.,0.));
#59592=CARTESIAN_POINT('',(0.,0.,0.));
#59593=CARTESIAN_POINT('Origin',(0.,0.,4.));
#59594=CARTESIAN_POINT('',(-4.51054691465169,-0.000515110389415763,0.38741669750802));
#59595=CARTESIAN_POINT('',(-4.51874859034235,-0.000597354552748235,0.112583302491978));
#59596=CARTESIAN_POINT('',(-4.51775,5.53264807684796E-16,4.));
#59597=CARTESIAN_POINT('',(-3.43378788736191,2.93584158412995,0.));
#59598=CARTESIAN_POINT('Ctrl Pts',(-4.51874859034235,-0.000597354552748235,
0.112583302491978));
#59599=CARTESIAN_POINT('Ctrl Pts',(-4.51722457181931,0.322607764342177,
0.101221950551661));
#59600=CARTESIAN_POINT('Ctrl Pts',(-4.48139903614817,0.645891255334514,
0.0898605986113441));
#59601=CARTESIAN_POINT('Ctrl Pts',(-4.41220310426637,0.961201691623003,
0.0784992466710271));
#59602=CARTESIAN_POINT('Ctrl Pts',(-4.25283743035848,1.68739554150353,0.0523328311140182));
#59603=CARTESIAN_POINT('Ctrl Pts',(-3.91646501574702,2.37129788193745,0.0261664155570086));
#59604=CARTESIAN_POINT('Ctrl Pts',(-3.43378788736191,2.93584158412995,-2.08166817117217E-16));
#59605=CARTESIAN_POINT('',(3.44055068766013,2.93810645203836,-8.32667268468867E-16));
#59606=CARTESIAN_POINT('Origin',(0.,0.,0.));
#59607=CARTESIAN_POINT('Ctrl Pts',(3.44055068766013,2.93810645203836,-8.32667268468867E-16));
#59608=CARTESIAN_POINT('Ctrl Pts',(2.51857754810217,4.00873567447971,0.0500251109657056));
#59609=CARTESIAN_POINT('Ctrl Pts',(1.04980798302248,4.62287274287841,0.10005022193141));
#59610=CARTESIAN_POINT('Ctrl Pts',(-0.359976603224271,4.51112404046721,
0.150075332897117));
#59611=CARTESIAN_POINT('Ctrl Pts',(-1.83479629347494,4.39422023240758,0.202408164011137));
#59612=CARTESIAN_POINT('Ctrl Pts',(-3.24506337966313,3.48291388857057,0.254740995125157));
#59613=CARTESIAN_POINT('Ctrl Pts',(-3.96016577839605,2.18804786800098,0.307073826239177));
#59614=CARTESIAN_POINT('Ctrl Pts',(-4.32611438556047,1.52540931786942,0.333854783328791));
#59615=CARTESIAN_POINT('Ctrl Pts',(-4.5100126795522,0.762323836917479,0.360635740418406));
#59616=CARTESIAN_POINT('Ctrl Pts',(-4.51054691465169,-0.000515110389415763,
0.38741669750802));
#59617=CARTESIAN_POINT('Origin',(0.,0.,4.));
#59618=CARTESIAN_POINT('',(-4.52244050167421,-0.00276900106626683,1.38741669750802));
#59619=CARTESIAN_POINT('',(-4.5233994151039,0.0021134167823725,1.11258330249198));
#59620=CARTESIAN_POINT('',(-4.51775,5.53264807684796E-16,4.));
#59621=CARTESIAN_POINT('Ctrl Pts',(-4.5233994151039,0.0021134167823725,
1.11258330249198));
#59622=CARTESIAN_POINT('Ctrl Pts',(-4.52416026905118,0.130280331830068,
1.10805201945945));
#59623=CARTESIAN_POINT('Ctrl Pts',(-4.51917716893618,0.258387747461467,
1.10352073642693));
#59624=CARTESIAN_POINT('Ctrl Pts',(-4.50825644670978,0.385987082702882,
1.0989894533944));
#59625=CARTESIAN_POINT('Ctrl Pts',(-4.38213051111597,1.85966118637707,1.04665662228038));
#59626=CARTESIAN_POINT('Ctrl Pts',(-3.46401651516602,3.2655651297045,0.994323791166365));
#59627=CARTESIAN_POINT('Ctrl Pts',(-2.16517718342927,3.97324079579977,0.941990960052346));
#59628=CARTESIAN_POINT('Ctrl Pts',(-0.866337851692522,4.68091646189503,
0.889658128938326));
#59629=CARTESIAN_POINT('Ctrl Pts',(0.813226815831038,4.69036385075812,0.837325297824306));
#59630=CARTESIAN_POINT('Ctrl Pts',(2.11977950774785,3.99758999513324,0.784992466710287));
#59631=CARTESIAN_POINT('Ctrl Pts',(3.42633219966466,3.30481613950837,0.732659635596268));
#59632=CARTESIAN_POINT('Ctrl Pts',(4.35987291597477,1.90982103939552,0.680326804482248));
#59633=CARTESIAN_POINT('Ctrl Pts',(4.50321991349222,0.437577595733461,0.627993973368229));
#59634=CARTESIAN_POINT('Ctrl Pts',(4.64656691100967,-1.0346658479286,0.57566114225421));
#59635=CARTESIAN_POINT('Ctrl Pts',(3.99972018973448,-2.58415763513987,0.523328311140192));
#59636=CARTESIAN_POINT('Ctrl Pts',(2.85003205531654,-3.51527160715898,0.470995480026173));
#59637=CARTESIAN_POINT('Ctrl Pts',(1.7003439208986,-4.4463855791781,0.418662648912154));
#59638=CARTESIAN_POINT('Ctrl Pts',(0.0478143733379097,-4.75912173600502,
0.366329817798135));
#59639=CARTESIAN_POINT('Ctrl Pts',(-1.36123648115533,-4.3152078830999,0.313996986684115));
#59640=CARTESIAN_POINT('Ctrl Pts',(-2.77028733564855,-3.87129403019478,
0.261664155570096));
#59641=CARTESIAN_POINT('Ctrl Pts',(-3.93585949707434,-2.67073016755762,
0.209331324456076));
#59642=CARTESIAN_POINT('Ctrl Pts',(-4.34790497327718,-1.24589506757571,
0.156998493342058));
#59643=CARTESIAN_POINT('Ctrl Pts',(-4.46447347068682,-0.842806340108052,
0.142193429725364));
#59644=CARTESIAN_POINT('Ctrl Pts',(-4.52073455040284,-0.421768388741025,
0.127388366108671));
#59645=CARTESIAN_POINT('Ctrl Pts',(-4.51874859034235,-0.000597354552748235,
0.112583302491978));
#59646=CARTESIAN_POINT('Ctrl Pts',(-4.51054691465169,-0.000515110389415763,
0.38741669750802));
#59647=CARTESIAN_POINT('Ctrl Pts',(-4.51105663160901,-0.728344389129203,
0.412968571532425));
#59648=CARTESIAN_POINT('Ctrl Pts',(-4.3446466691941,-1.4559492437521,0.438520445556829));
#59649=CARTESIAN_POINT('Ctrl Pts',(-4.01017598625922,-2.09587333886935,
0.464072319581234));
#59650=CARTESIAN_POINT('Ctrl Pts',(-3.32514608411178,-3.40650282786799,
0.516405150695253));
#59651=CARTESIAN_POINT('Ctrl Pts',(-1.9351485685392,-4.34933610856308,0.568737981809272));
#59652=CARTESIAN_POINT('Ctrl Pts',(-0.463832664911,-4.50105515886306,0.621070812923292));
#59653=CARTESIAN_POINT('Ctrl Pts',(1.00748323871719,-4.65277420916302,0.673403644037311));
#59654=CARTESIAN_POINT('Ctrl Pts',(2.560117530401,-4.01337902906788,0.725736475151331));
#59655=CARTESIAN_POINT('Ctrl Pts',(3.49818631344856,-2.86985357730659,0.77806930626535));
#59656=CARTESIAN_POINT('Ctrl Pts',(4.43625509649613,-1.7263281255453,0.830402137379369));
#59657=CARTESIAN_POINT('Ctrl Pts',(4.75975837090746,-0.0786724021178761,
0.882734968493387));
#59658=CARTESIAN_POINT('Ctrl Pts',(4.32353285348464,1.33455667095541,0.935067799607406));
#59659=CARTESIAN_POINT('Ctrl Pts',(3.88730733606183,2.7477857440287,0.987400630721425));
#59660=CARTESIAN_POINT('Ctrl Pts',(2.69135302680487,3.92658816674785,1.03973346183545));
#59661=CARTESIAN_POINT('Ctrl Pts',(1.27193499135498,4.34236723513978,1.09206629294946));
#59662=CARTESIAN_POINT('Ctrl Pts',(-0.147483044094926,4.7581463035317,1.14439912406348));
#59663=CARTESIAN_POINT('Ctrl Pts',(-1.79036480573777,4.41090201759639,1.1967319551775));
#59664=CARTESIAN_POINT('Ctrl Pts',(-2.92016350112278,3.45636436650575,1.24906478629152));
#59665=CARTESIAN_POINT('Ctrl Pts',(-3.91577693325848,2.61519636835964,1.29518209003036));
#59666=CARTESIAN_POINT('Ctrl Pts',(-4.51294659780824,1.30242392182032,1.34129939376919));
#59667=CARTESIAN_POINT('Ctrl Pts',(-4.52244050167421,-0.00276900106626683,
1.38741669750802));
#59668=CARTESIAN_POINT('Origin',(0.,0.,4.));
#59669=CARTESIAN_POINT('',(-4.51698911071085,0.00388851918503852,2.38741669750802));
#59670=CARTESIAN_POINT('',(-4.51093362149631,0.00101330851266679,2.11258330249198));
#59671=CARTESIAN_POINT('',(-4.51775,5.53264807684796E-16,4.));
#59672=CARTESIAN_POINT('Ctrl Pts',(-4.51093362149631,0.00101330851266679,
2.11258330249198));
#59673=CARTESIAN_POINT('Ctrl Pts',(-4.51232811703185,0.680923530020972,
2.08871567281024));
#59674=CARTESIAN_POINT('Ctrl Pts',(-4.36790019846314,1.36027124256301,2.06484804312849));
#59675=CARTESIAN_POINT('Ctrl Pts',(-4.07455659430891,1.96770381197164,2.04098041344675));
#59676=CARTESIAN_POINT('Ctrl Pts',(-3.43136321904367,3.29957742036487,1.98864758233273));
#59677=CARTESIAN_POINT('Ctrl Pts',(-2.07224023608874,4.28571055146719,1.93631475121871));
#59678=CARTESIAN_POINT('Ctrl Pts',(-0.606537899693793,4.48397159897241,
1.88398192010469));
#59679=CARTESIAN_POINT('Ctrl Pts',(0.859164436701136,4.68223264647763,1.83164908899067));
#59680=CARTESIAN_POINT('Ctrl Pts',(2.43144612653608,4.09262161038578,1.77931625787665));
#59681=CARTESIAN_POINT('Ctrl Pts',(3.40536636602181,2.97949323501332,1.72698342676264));
#59682=CARTESIAN_POINT('Ctrl Pts',(4.37928660550757,1.86636485964083,1.67465059564862));
#59683=CARTESIAN_POINT('Ctrl Pts',(4.75484539464409,0.229719144987712,1.6223177645346));
#59684=CARTESIAN_POINT('Ctrl Pts',(4.36368967023442,-1.19666928711504,1.56998493342058));
#59685=CARTESIAN_POINT('Ctrl Pts',(3.97253394582476,-2.62305771921779,1.51765210230656));
#59686=CARTESIAN_POINT('Ctrl Pts',(2.81466370786892,-3.83918886877017,1.46531927119254));
#59687=CARTESIAN_POINT('Ctrl Pts',(1.40915332177568,-4.29979703199479,1.41298644007852));
#59688=CARTESIAN_POINT('Ctrl Pts',(0.00364293568242802,-4.76040519521942,
1.3606536089645));
#59689=CARTESIAN_POINT('Ctrl Pts',(-1.64950759854823,-4.46549037211628,
1.30832077785048));
#59690=CARTESIAN_POINT('Ctrl Pts',(-2.80901392804473,-3.54731082855424,
1.25598794673646));
#59691=CARTESIAN_POINT('Ctrl Pts',(-3.86812340827646,-2.70863264767388,
1.20818639865497));
#59692=CARTESIAN_POINT('Ctrl Pts',(-4.51537299162016,-1.34994888171753,
1.16038485057347));
#59693=CARTESIAN_POINT('Ctrl Pts',(-4.5233994151039,0.0021134167823725,
1.11258330249198));
#59694=CARTESIAN_POINT('Ctrl Pts',(-4.52244050167421,-0.00276900106626683,
1.38741669750802));
#59695=CARTESIAN_POINT('Ctrl Pts',(-4.52372005651789,-0.178678295071038,
1.39363222488321));
#59696=CARTESIAN_POINT('Ctrl Pts',(-4.51432465941186,-0.35444990932754,
1.39984775225839));
#59697=CARTESIAN_POINT('Ctrl Pts',(-4.49379103756964,-0.528910718243546,
1.40606327963358));
#59698=CARTESIAN_POINT('Ctrl Pts',(-4.32090424950433,-1.99781713565632,
1.4583961107476));
#59699=CARTESIAN_POINT('Ctrl Pts',(-3.3584150442465,-3.37379895423595,1.51072894186162));
#59700=CARTESIAN_POINT('Ctrl Pts',(-2.037860803389,-4.0399278796399,1.56306177297564));
#59701=CARTESIAN_POINT('Ctrl Pts',(-0.717306562531505,-4.70605680504386,
1.61539460408966));
#59702=CARTESIAN_POINT('Ctrl Pts',(0.961312713925656,-4.66233283727215,
1.66772743520368));
#59703=CARTESIAN_POINT('Ctrl Pts',(2.24539906972787,-3.92836571897045,1.72006026631769));
#59704=CARTESIAN_POINT('Ctrl Pts',(3.52948542553009,-3.19439860066874,1.77239309743171));
#59705=CARTESIAN_POINT('Ctrl Pts',(4.41903886067735,-1.77018833183704,1.82472592854573));
#59706=CARTESIAN_POINT('Ctrl Pts',(4.51522900816629,-0.294270957708535,
1.87705875965975));
#59707=CARTESIAN_POINT('Ctrl Pts',(4.61141915565522,1.18164641641996,1.92939159077377));
#59708=CARTESIAN_POINT('Ctrl Pts',(3.91424601548584,2.70927089584527,1.98172442188779));
#59709=CARTESIAN_POINT('Ctrl Pts',(2.73628580760446,3.60369609834798,2.03405725300181));
#59710=CARTESIAN_POINT('Ctrl Pts',(1.55832559972309,4.4981213008507,2.08639008411583));
#59711=CARTESIAN_POINT('Ctrl Pts',(-0.100421675870265,4.75934722643081,
2.13872291522985));
#59712=CARTESIAN_POINT('Ctrl Pts',(-1.49626358664302,4.2702551012346,2.19105574634387));
#59713=CARTESIAN_POINT('Ctrl Pts',(-2.89210549741577,3.78116297603839,2.24338857745789));
#59714=CARTESIAN_POINT('Ctrl Pts',(-4.02504204336792,2.54175280006585,2.29572140857191));
#59715=CARTESIAN_POINT('Ctrl Pts',(-4.38712504707582,1.10770899592287,2.34805423968593));
#59716=CARTESIAN_POINT('Ctrl Pts',(-4.47790602629514,0.748167400624681,
2.36117505895996));
#59717=CARTESIAN_POINT('Ctrl Pts',(-4.52023125554896,0.376391161643011,
2.37429587823399));
#59718=CARTESIAN_POINT('Ctrl Pts',(-4.51698911071085,0.00388851918503852,
2.38741669750802));
#59719=CARTESIAN_POINT('Origin',(0.,0.,4.));
#59720=CARTESIAN_POINT('',(-4.51234492774861,-0.00257476452032779,3.38741669750802));
#59721=CARTESIAN_POINT('',(-4.52027081060448,-0.00355576929457683,3.11258330249198));
#59722=CARTESIAN_POINT('',(-4.51775,5.53264807684796E-16,4.));
#59723=CARTESIAN_POINT('Ctrl Pts',(-4.52027081060448,-0.00355576929457683,
3.11258330249198));
#59724=CARTESIAN_POINT('Ctrl Pts',(-4.50971003274407,1.22072076070225,3.06937932616102));
#59725=CARTESIAN_POINT('Ctrl Pts',(-3.99354051828841,2.45284880293372,3.02617534983006));
#59726=CARTESIAN_POINT('Ctrl Pts',(-3.10547711214626,3.29088013555457,2.9829713734991));
#59727=CARTESIAN_POINT('Ctrl Pts',(-2.02976889732455,4.30598466811756,2.93063854238508));
#59728=CARTESIAN_POINT('Ctrl Pts',(-0.408403261408893,4.74285492731681,
2.87830571127106));
#59729=CARTESIAN_POINT('Ctrl Pts',(1.03168676818161,4.40562172719721,2.82597288015704));
#59730=CARTESIAN_POINT('Ctrl Pts',(2.4717767977721,4.06838852707761,2.77364004904302));
#59731=CARTESIAN_POINT('Ctrl Pts',(3.73059122103745,2.95705186763916,2.721307217929));
#59732=CARTESIAN_POINT('Ctrl Pts',(4.2437450475446,1.56987545160024,2.66897438681498));
#59733=CARTESIAN_POINT('Ctrl Pts',(4.75689887405174,0.182699035561331,2.61664155570096));
#59734=CARTESIAN_POINT('Ctrl Pts',(4.5243921038007,-1.48031713707804,2.56430872458694));
#59735=CARTESIAN_POINT('Ctrl Pts',(3.65046881853353,-2.67356621578173,2.51197589347292));
#59736=CARTESIAN_POINT('Ctrl Pts',(2.77654553326636,-3.86681529448543,2.4596430623589));
#59737=CARTESIAN_POINT('Ctrl Pts',(1.26120573298304,-4.59029727925343,2.40731023124489));
#59738=CARTESIAN_POINT('Ctrl Pts',(-0.216154740062777,-4.51964138893216,
2.35497740013087));
#59739=CARTESIAN_POINT('Ctrl Pts',(-1.69351521310859,-4.44898549861089,
2.30264456901685));
#59740=CARTESIAN_POINT('Ctrl Pts',(-3.1328963589169,-3.58419173320037,2.25031173790283));
#59741=CARTESIAN_POINT('Ctrl Pts',(-3.88895504803329,-2.31298780765304,
2.19797890678881));
#59742=CARTESIAN_POINT('Ctrl Pts',(-4.30019522790109,-1.62154660273587,
2.16951370535653));
#59743=CARTESIAN_POINT('Ctrl Pts',(-4.50927050719276,-0.809866601606811,
2.14104850392425));
#59744=CARTESIAN_POINT('Ctrl Pts',(-4.51093362149631,0.00101330851266679,
2.11258330249198));
#59745=CARTESIAN_POINT('Ctrl Pts',(-4.51698911071085,0.00388851918503852,
2.38741669750802));
#59746=CARTESIAN_POINT('Ctrl Pts',(-4.50729985128856,-1.10934821713655,
2.42662870934801));
#59747=CARTESIAN_POINT('Ctrl Pts',(-4.09063314279102,-2.22907270570801,
2.465840721188));
#59748=CARTESIAN_POINT('Ctrl Pts',(-3.34408434212355,-3.04811166820345,
2.50505273302798));
#59749=CARTESIAN_POINT('Ctrl Pts',(-2.34773117199973,-4.14121109587334,
2.557385564142));
#59750=CARTESIAN_POINT('Ctrl Pts',(-0.763795370288439,-4.69873251889968,
2.60971839525602));
#59751=CARTESIAN_POINT('Ctrl Pts',(0.697571505631126,-4.4707134324377,2.66205122637004));
#59752=CARTESIAN_POINT('Ctrl Pts',(2.15893838155069,-4.24269434597572,2.71438405748406));
#59753=CARTESIAN_POINT('Ctrl Pts',(3.49773633167853,-3.2291347500254,2.76671688859808));
#59754=CARTESIAN_POINT('Ctrl Pts',(4.11372028899329,-1.88446020659954,2.8190497197121));
#59755=CARTESIAN_POINT('Ctrl Pts',(4.72970424630805,-0.539785663173669,
2.87138255082612));
#59756=CARTESIAN_POINT('Ctrl Pts',(4.62287421080972,1.13600382772776,2.92371538194014));
#59757=CARTESIAN_POINT('Ctrl Pts',(3.84112705187867,2.39157432571858,2.97604821305416));
#59758=CARTESIAN_POINT('Ctrl Pts',(3.05937989294762,3.6471448237094,3.02838104416818));
#59759=CARTESIAN_POINT('Ctrl Pts',(1.60271561058387,4.48249632878962,3.08071387528219));
#59760=CARTESIAN_POINT('Ctrl Pts',(0.124224136080841,4.52310215772866,3.13304670639621));
#59761=CARTESIAN_POINT('Ctrl Pts',(-1.35426733842219,4.56370798666771,3.18537953751023));
#59762=CARTESIAN_POINT('Ctrl Pts',(-2.85458600506451,3.80956813946558,3.23771236862425));
#59763=CARTESIAN_POINT('Ctrl Pts',(-3.70406963378462,2.5987983669013,3.29004519973827));
#59764=CARTESIAN_POINT('Ctrl Pts',(-4.2309249653141,1.84787099365534,3.32250236566152));
#59765=CARTESIAN_POINT('Ctrl Pts',(-4.50743256748542,0.921298090727453,
3.35495953158477));
#59766=CARTESIAN_POINT('Ctrl Pts',(-4.51234492774861,-0.00257476452032779,
3.38741669750802));
#59767=CARTESIAN_POINT('Origin',(0.,0.,4.));
#59768=CARTESIAN_POINT('',(-4.52478583629221,-0.000271302356462328,4.38741669750802));
#59769=CARTESIAN_POINT('',(-4.51939464917808,0.00373292266216646,4.11258330249198));
#59770=CARTESIAN_POINT('',(-4.51775,5.53264807684796E-16,4.));
#59771=CARTESIAN_POINT('Ctrl Pts',(-4.51939464917808,0.00373292266216647,
4.11258330249198));
#59772=CARTESIAN_POINT('Ctrl Pts',(-4.52195179175284,0.293129143485266,
4.10237581062582));
#59773=CARTESIAN_POINT('Ctrl Pts',(-4.49647546580418,0.582077227182858,
4.09216831875966));
#59774=CARTESIAN_POINT('Ctrl Pts',(-4.44131034778915,0.865241438283023,
4.0819608268935));
#59775=CARTESIAN_POINT('Ctrl Pts',(-4.15848408230504,2.31699717136045,4.02962799577948));
#59776=CARTESIAN_POINT('Ctrl Pts',(-3.09528361658689,3.61672297535275,3.97729516466546));
#59777=CARTESIAN_POINT('Ctrl Pts',(-1.72839087618034,4.18169168234348,3.92496233355144));
#59778=CARTESIAN_POINT('Ctrl Pts',(-0.361498135773788,4.7466603893342,3.87262950243742));
#59779=CARTESIAN_POINT('Ctrl Pts',(1.30908687932117,4.57687199932334,3.8202966713234));
#59780=CARTESIAN_POINT('Ctrl Pts',(2.5343636726828,3.74845049626232,3.76796384020938));
#59781=CARTESIAN_POINT('Ctrl Pts',(3.75964046604444,2.9200289932013,3.71563100909536));
#59782=CARTESIAN_POINT('Ctrl Pts',(4.53960903767275,1.43297437709012,3.66329817798134));
#59783=CARTESIAN_POINT('Ctrl Pts',(4.52457341059044,-0.0459980138823182,
3.61096534686733));
#59784=CARTESIAN_POINT('Ctrl Pts',(4.50953778350813,-1.52497040485477,3.55863251575331));
#59785=CARTESIAN_POINT('Ctrl Pts',(3.69949795771518,-2.99586057068848,3.50629968463929));
#59786=CARTESIAN_POINT('Ctrl Pts',(2.45763224901275,-3.79920044943065,3.45396685352527));
#59787=CARTESIAN_POINT('Ctrl Pts',(1.21576654031032,-4.60254032817281,3.40163402241125));
#59788=CARTESIAN_POINT('Ctrl Pts',(-0.457925051301578,-4.73832991982345,
3.34930119129723));
#59789=CARTESIAN_POINT('Ctrl Pts',(-1.81304922569253,-4.1456884652134,3.29696836018321));
#59790=CARTESIAN_POINT('Ctrl Pts',(-3.16817340008348,-3.55304701060334,
3.24463552906919));
#59791=CARTESIAN_POINT('Ctrl Pts',(-4.20473015725347,-2.23197450973259,
3.19230269795517));
#59792=CARTESIAN_POINT('Ctrl Pts',(-4.45798313897459,-0.774768856333857,
3.13996986684115));
#59793=CARTESIAN_POINT('Ctrl Pts',(-4.50216018126897,-0.520576248830078,
3.1308410120581));
#59794=CARTESIAN_POINT('Ctrl Pts',(-4.52250226742098,-0.262241279420579,
3.12171215727504));
#59795=CARTESIAN_POINT('Ctrl Pts',(-4.52027081060448,-0.00355576929457683,
3.11258330249198));
#59796=CARTESIAN_POINT('Ctrl Pts',(-4.51234492774861,-0.00257476452032779,
3.38741669750802));
#59797=CARTESIAN_POINT('Ctrl Pts',(-4.51535309020244,-0.568323098591327,
3.40729236269879));
#59798=CARTESIAN_POINT('Ctrl Pts',(-4.41651517435603,-1.13305893603127,
3.42716802788956));
#59799=CARTESIAN_POINT('Ctrl Pts',(-4.21095206217547,-1.65582834772821,
3.44704369308033));
#59800=CARTESIAN_POINT('Ctrl Pts',(-3.66970227104832,-3.032285591867,3.49937652419435));
#59801=CARTESIAN_POINT('Ctrl Pts',(-2.3885540979961,-4.11780038221814,3.55170935530837));
#59802=CARTESIAN_POINT('Ctrl Pts',(-0.941905499312602,-4.42568625369714,
3.60404218642239));
#59803=CARTESIAN_POINT('Ctrl Pts',(0.504743099370899,-4.73357212517614,
3.65637501753641));
#59804=CARTESIAN_POINT('Ctrl Pts',(2.11689212368568,-4.263829077783,3.70870784865043));
#59805=CARTESIAN_POINT('Ctrl Pts',(3.17174063018436,-3.22706463608245,3.76104067976445));
#59806=CARTESIAN_POINT('Ctrl Pts',(4.22658913668306,-2.19030019438189,3.81337351087847));
#59807=CARTESIAN_POINT('Ctrl Pts',(4.72413712536563,-0.586514358373886,
3.86570634199248));
#59808=CARTESIAN_POINT('Ctrl Pts',(4.44131082922502,0.865241532073468,3.9180391731065));
#59809=CARTESIAN_POINT('Ctrl Pts',(4.15848453308441,2.31699742252081,3.97037200422052));
#59810=CARTESIAN_POINT('Ctrl Pts',(3.09528395212065,3.61672336740751,4.02270483533454));
#59811=CARTESIAN_POINT('Ctrl Pts',(1.7283910635404,4.18169213563993,4.07503766644856));
#59812=CARTESIAN_POINT('Ctrl Pts',(0.361498174960155,4.74666090387236,4.12737049756258));
#59813=CARTESIAN_POINT('Ctrl Pts',(-1.30908702123658,4.5768724954505,4.1797033286766));
#59814=CARTESIAN_POINT('Ctrl Pts',(-2.5343639474132,3.74845090259061,4.23203615979062));
#59815=CARTESIAN_POINT('Ctrl Pts',(-3.74701372251171,2.9285666488301,4.28382967236309));
#59816=CARTESIAN_POINT('Ctrl Pts',(-4.52348622608021,1.46355441369542,4.33562318493555));
#59817=CARTESIAN_POINT('Ctrl Pts',(-4.52478583629221,-0.000271302356462328,
4.38741669750802));
#59818=CARTESIAN_POINT('Origin',(0.,0.,4.));
#59819=CARTESIAN_POINT('',(-4.51292607061429,0.0029183530353194,5.38741669750802));
#59820=CARTESIAN_POINT('',(-4.51119223387812,-0.00146992377155156,5.11258330249198));
#59821=CARTESIAN_POINT('',(-4.51775,5.53264807684796E-16,4.));
#59822=CARTESIAN_POINT('Ctrl Pts',(-4.51119223387812,-0.00146992377155156,
5.11258330249198));
#59823=CARTESIAN_POINT('Ctrl Pts',(-4.50867979289825,0.840016500418339,
5.0830394639766));
#59824=CARTESIAN_POINT('Ctrl Pts',(-4.28245206788243,1.68275768437228,5.05349562546122));
#59825=CARTESIAN_POINT('Ctrl Pts',(-3.84112663548136,2.39157406650585,5.02395178694585));
#59826=CARTESIAN_POINT('Ctrl Pts',(-3.05937956127687,3.64714442841863,4.97161895583183));
#59827=CARTESIAN_POINT('Ctrl Pts',(-1.60271543685273,4.48249584288365,4.9192861247178));
#59828=CARTESIAN_POINT('Ctrl Pts',(-0.124224122626221,4.52310166740692,
4.86695329360379));
#59829=CARTESIAN_POINT('Ctrl Pts',(1.3542671916003,4.56370749193019,4.81462046248977));
#59830=CARTESIAN_POINT('Ctrl Pts',(2.85458569562921,3.80956772651169,4.76228763137575));
#59831=CARTESIAN_POINT('Ctrl Pts',(3.70406923227031,2.59879808520239,4.70995480026173));
#59832=CARTESIAN_POINT('Ctrl Pts',(4.5535527689114,1.3880284438931,4.65762196914771));
#59833=CARTESIAN_POINT('Ctrl Pts',(4.7522013381647,-0.279371073306991,4.60528913803369));
#59834=CARTESIAN_POINT('Ctrl Pts',(4.21095160570608,-1.65582816824236,4.55295630691967));
#59835=CARTESIAN_POINT('Ctrl Pts',(3.66970187324747,-3.03228526317774,4.50062347580565));
#59836=CARTESIAN_POINT('Ctrl Pts',(2.38855383907694,-4.11779993584839,4.44829064469163));
#59837=CARTESIAN_POINT('Ctrl Pts',(0.94190539721171,-4.42568577395046,4.39595781357761));
#59838=CARTESIAN_POINT('Ctrl Pts',(-0.50474304465354,-4.73357161205254,
4.34362498246359));
#59839=CARTESIAN_POINT('Ctrl Pts',(-2.11689189421349,-4.263828615586,4.29129215134958));
#59840=CARTESIAN_POINT('Ctrl Pts',(-3.17174028636843,-3.22706428627144,
4.23895932023556));
#59841=CARTESIAN_POINT('Ctrl Pts',(-4.02084104068784,-2.3925203076111,4.1968339809877));
#59842=CARTESIAN_POINT('Ctrl Pts',(-4.50884156719875,-1.19057750531243,
4.15470864173984));
#59843=CARTESIAN_POINT('Ctrl Pts',(-4.51939464917808,0.00373292266216647,
4.11258330249198));
#59844=CARTESIAN_POINT('Ctrl Pts',(-4.52478583629221,-0.000271302356462328,
4.38741669750802));
#59845=CARTESIAN_POINT('Ctrl Pts',(-4.52479936895005,-0.0155139130822968,
4.38795601604957));
#59846=CARTESIAN_POINT('Ctrl Pts',(-4.52472885144687,-0.030756395156677,
4.38849533459112));
#59847=CARTESIAN_POINT('Ctrl Pts',(-4.52457390104248,-0.0459980188636215,
4.38903465313267));
#59848=CARTESIAN_POINT('Ctrl Pts',(-4.50953827233865,-1.52497057016008,
4.44136748424669));
#59849=CARTESIAN_POINT('Ctrl Pts',(-3.69949835877446,-2.99586089545507,
4.49370031536071));
#59850=CARTESIAN_POINT('Ctrl Pts',(-2.45763251543912,-3.79920086127216,
4.54603314647473));
#59851=CARTESIAN_POINT('Ctrl Pts',(-1.21576667210378,-4.60254082708924,
4.59836597758875));
#59852=CARTESIAN_POINT('Ctrl Pts',(0.45792510100271,-4.73833043342844,4.65069880870277));
#59853=CARTESIAN_POINT('Ctrl Pts',(1.81304942226226,-4.14568891458885,4.70303163981679));
#59854=CARTESIAN_POINT('Ctrl Pts',(3.16817374352182,-3.55304739574926,4.75536447093081));
#59855=CARTESIAN_POINT('Ctrl Pts',(4.20473061293445,-2.23197475173087,4.80769730204483));
#59856=CARTESIAN_POINT('Ctrl Pts',(4.45798362215519,-0.774768940348221,
4.86003013315885));
#59857=CARTESIAN_POINT('Ctrl Pts',(4.71123663137592,0.682436871034428,4.91236296427287));
#59858=CARTESIAN_POINT('Ctrl Pts',(4.18118578040478,2.27577584978132,4.96469579538688));
#59859=CARTESIAN_POINT('Ctrl Pts',(3.10547744889356,3.29088049233953,5.0170286265009));
#59860=CARTESIAN_POINT('Ctrl Pts',(2.02976911738235,4.30598513489774,5.06936145761492));
#59861=CARTESIAN_POINT('Ctrl Pts',(0.408403305331062,4.74285544126724,5.12169428872895));
#59862=CARTESIAN_POINT('Ctrl Pts',(-1.03168688021991,4.40562220466712,5.17402711984297));
#59863=CARTESIAN_POINT('Ctrl Pts',(-2.47177706577088,4.068388968067,5.22635995095699));
#59864=CARTESIAN_POINT('Ctrl Pts',(-3.73059162482154,2.95705218849725,5.278692782071));
#59865=CARTESIAN_POINT('Ctrl Pts',(-4.2437455072054,1.56987562195304,5.33102561318502));
#59866=CARTESIAN_POINT('Ctrl Pts',(-4.42806131327582,1.07162631350615,5.34982264129268));
#59867=CARTESIAN_POINT('Ctrl Pts',(-4.51617798535533,0.537790377713164,
5.36861966940035));
#59868=CARTESIAN_POINT('Ctrl Pts',(-4.51292607061429,0.0029183530353194,
5.38741669750802));
#59869=CARTESIAN_POINT('Origin',(0.,0.,4.));
#59870=CARTESIAN_POINT('',(-4.51611343680291,-0.0038242599945422,6.38741669750802));
#59871=CARTESIAN_POINT('',(-4.52399690261043,-0.00167256832429505,6.11258330249198));
#59872=CARTESIAN_POINT('',(-4.51775,5.53264807684796E-16,4.));
#59873=CARTESIAN_POINT('Ctrl Pts',(-4.52399690261043,-0.00167256832429505,
6.11258330249198));
#59874=CARTESIAN_POINT('Ctrl Pts',(-4.5173342997898,1.3804594726294,6.06370311732738));
#59875=CARTESIAN_POINT('Ctrl Pts',(-3.83652995787924,2.76828008382611,6.01482293216279));
#59876=CARTESIAN_POINT('Ctrl Pts',(-2.73628551041168,3.60369570881218,5.96594274699819));
#59877=CARTESIAN_POINT('Ctrl Pts',(-1.55832542986843,4.49812081512447,5.91360991588417));
#59878=CARTESIAN_POINT('Ctrl Pts',(0.100421664862097,4.75934671033683,5.86127708477015));
#59879=CARTESIAN_POINT('Ctrl Pts',(1.49626342410919,4.27025463771519,5.80894425365613));
#59880=CARTESIAN_POINT('Ctrl Pts',(2.89210518335629,3.78116256509354,5.75661142254211));
#59881=CARTESIAN_POINT('Ctrl Pts',(4.02504160711995,2.54175252463788,5.7042785914281));
#59882=CARTESIAN_POINT('Ctrl Pts',(4.3871245717083,1.10770887619882,5.65194576031408));
#59883=CARTESIAN_POINT('Ctrl Pts',(4.74920753629665,-0.326334772240243,
5.59961292920006));
#59884=CARTESIAN_POINT('Ctrl Pts',(4.34043704170966,-1.95501202866272,5.54728009808604));
#59885=CARTESIAN_POINT('Ctrl Pts',(3.34408397951354,-3.04811133798521,5.49494726697202));
#59886=CARTESIAN_POINT('Ctrl Pts',(2.34773091731743,-4.14121064730769,5.442614435858));
#59887=CARTESIAN_POINT('Ctrl Pts',(0.763795287512193,-4.6987320095302,5.39028160474398));
#59888=CARTESIAN_POINT('Ctrl Pts',(-0.697571429950846,-4.47071294770401,
5.33794877362996));
#59889=CARTESIAN_POINT('Ctrl Pts',(-2.15893814741389,-4.24269388587781,
5.28561594251594));
#59890=CARTESIAN_POINT('Ctrl Pts',(-3.49773595253472,-3.22913440000291,
5.23328311140192));
#59891=CARTESIAN_POINT('Ctrl Pts',(-4.11371984310272,-1.88446000238519,
5.1809502802879));
#59892=CARTESIAN_POINT('Ctrl Pts',(-4.3819578119688,-1.29890454431857,5.15816128768926));
#59893=CARTESIAN_POINT('Ctrl Pts',(-4.51313023522704,-0.650560524599824,
5.13537229509062));
#59894=CARTESIAN_POINT('Ctrl Pts',(-4.51119223387812,-0.00146992377155156,
5.11258330249198));
#59895=CARTESIAN_POINT('Ctrl Pts',(-4.51292607061429,0.0029183530353194,
5.38741669750802));
#59896=CARTESIAN_POINT('Ctrl Pts',(-4.50712432517217,-0.95134754210846,
5.42095250051437));
#59897=CARTESIAN_POINT('Ctrl Pts',(-4.21049476107502,-1.90891132639337,
5.45448830352073));
#59898=CARTESIAN_POINT('Ctrl Pts',(-3.65046921487666,-2.67356650591896,
5.48802410652708));
#59899=CARTESIAN_POINT('Ctrl Pts',(-2.776545834447,-3.86681571372806,5.5403569376411));
#59900=CARTESIAN_POINT('Ctrl Pts',(-1.26120586787061,-4.5902977758276,5.59268976875511));
#59901=CARTESIAN_POINT('Ctrl Pts',(0.216154764597121,-4.51964187827841,
5.64502259986913));
#59902=CARTESIAN_POINT('Ctrl Pts',(1.69351539706486,-4.44898598072923,5.69735543098315));
#59903=CARTESIAN_POINT('Ctrl Pts',(3.13289669542393,-3.58419212353131,5.74968826209718));
#59904=CARTESIAN_POINT('Ctrl Pts',(3.88895546769304,-2.31298805942388,5.8020210932112));
#59905=CARTESIAN_POINT('Ctrl Pts',(4.64501423996215,-1.04178399531645,5.85435392432522));
#59906=CARTESIAN_POINT('Ctrl Pts',(4.71775048614129,0.635830275700497,5.90668675543923));
#59907=CARTESIAN_POINT('Ctrl Pts',(4.07455703922814,1.96770402713248,5.95901958655325));
#59908=CARTESIAN_POINT('Ctrl Pts',(3.43136359231499,3.29957777856446,6.01135241766727));
#59909=CARTESIAN_POINT('Ctrl Pts',(2.07224045230956,4.28571101041149,6.0636852487813));
#59910=CARTESIAN_POINT('Ctrl Pts',(0.606537960019231,4.4839720817303,6.11601807989532));
#59911=CARTESIAN_POINT('Ctrl Pts',(-0.859164532271093,4.68223315304911,
6.16835091100933));
#59912=CARTESIAN_POINT('Ctrl Pts',(-2.43144637684631,4.0926220638397,6.22068374212335));
#59913=CARTESIAN_POINT('Ctrl Pts',(-3.4053667262744,2.97949356381203,6.27301657323736));
#59914=CARTESIAN_POINT('Ctrl Pts',(-4.11503346658856,2.16838999191388,6.31114994799425));
#59915=CARTESIAN_POINT('Ctrl Pts',(-4.506994027605,1.07931947572563,6.34928332275114));
#59916=CARTESIAN_POINT('Ctrl Pts',(-4.51611343680291,-0.0038242599945422,
6.38741669750802));
#59917=CARTESIAN_POINT('Origin',(0.,0.,4.));
#59918=CARTESIAN_POINT('',(-4.52286359173795,0.00246468782935438,7.38741669750802));
#59919=CARTESIAN_POINT('',(-4.51483246697105,0.00361950456559231,7.11258330249198));
#59920=CARTESIAN_POINT('',(-4.51775,5.53264807684796E-16,4.));
#59921=CARTESIAN_POINT('',(3.43378788736184,2.93584158413003,8.));
#59922=CARTESIAN_POINT('Ctrl Pts',(-4.52286359173795,0.00246468782935438,
7.38741669750802));
#59923=CARTESIAN_POINT('Ctrl Pts',(-4.514736621556,-1.33289820095304,7.43461263832996));
#59924=CARTESIAN_POINT('Ctrl Pts',(-3.88687106704568,-2.67555385687553,
7.48180857915189));
#59925=CARTESIAN_POINT('Ctrl Pts',(-2.85003294005483,-3.51527175392636,
7.52900451997383));
#59926=CARTESIAN_POINT('Ctrl Pts',(-1.70034350389957,-4.44638604308903,
7.58133735108785));
#59927=CARTESIAN_POINT('Ctrl Pts',(-0.0478099810187527,-4.759123220785,
7.63367018220187));
#59928=CARTESIAN_POINT('Ctrl Pts',(1.3612375474742,-4.31520832020808,7.68600301331589));
#59929=CARTESIAN_POINT('Ctrl Pts',(2.77028507596716,-3.87129341963115,7.73833584442991));
#59930=CARTESIAN_POINT('Ctrl Pts',(3.93584661007225,-2.67072644078133,7.79066867554392));
#59931=CARTESIAN_POINT('Ctrl Pts',(4.34789968202776,-1.24589357093064,7.84300150665794));
#59932=CARTESIAN_POINT('Ctrl Pts',(4.55392621800552,-0.533477136005289,
7.86916792221495));
#59933=CARTESIAN_POINT('Ctrl Pts',(4.57157563844588,0.235005771670285,7.89533433777196));
#59934=CARTESIAN_POINT('Ctrl Pts',(4.41221033788124,0.961199526155991,7.92150075332897));
#59935=CARTESIAN_POINT('Ctrl Pts',(4.2528450373166,1.6873932806417,7.94766716888598));
#59936=CARTESIAN_POINT('Ctrl Pts',(3.91646501574697,2.37129788193754,7.97383358444299));
#59937=CARTESIAN_POINT('Ctrl Pts',(3.43378788736183,2.93584158413004,8.));
#59938=CARTESIAN_POINT('',(-3.44054916109511,2.9381068161154,8.));
#59939=CARTESIAN_POINT('Origin',(0.,0.,8.));
#59940=CARTESIAN_POINT('Ctrl Pts',(-3.44054916109511,2.9381068161154,8.));
#59941=CARTESIAN_POINT('Ctrl Pts',(-2.51857342159112,4.00873681403696,7.94997488903429));
#59942=CARTESIAN_POINT('Ctrl Pts',(-1.04980743191293,4.62287257548397,7.89994977806859));
#59943=CARTESIAN_POINT('Ctrl Pts',(0.359975956906261,4.51112341871505,7.84992466710289));
#59944=CARTESIAN_POINT('Ctrl Pts',(1.83479439449057,4.39421913533762,7.79759183598887));
#59945=CARTESIAN_POINT('Ctrl Pts',(3.24506283044465,3.48291324925361,7.74525900487485));
#59946=CARTESIAN_POINT('Ctrl Pts',(3.96016560277148,2.18804756351099,7.69292617376083));
#59947=CARTESIAN_POINT('Ctrl Pts',(4.67526837509831,0.893181877768381,7.64059334264681));
#59948=CARTESIAN_POINT('Ctrl Pts',(4.69520548379788,-0.785243607632836,
7.58826051153279));
#59949=CARTESIAN_POINT('Ctrl Pts',(4.01017546547555,-2.09587300826054,7.53592768041877));
#59950=CARTESIAN_POINT('Ctrl Pts',(3.32514544715321,-3.40650240888826,7.48359484930475));
#59951=CARTESIAN_POINT('Ctrl Pts',(1.93514830180898,-4.34933572474246,7.43126201819073));
#59952=CARTESIAN_POINT('Ctrl Pts',(0.463832634566904,-4.50105475907159,
7.37892918707671));
#59953=CARTESIAN_POINT('Ctrl Pts',(-1.00748303267517,-4.65277379340072,
7.32659635596269));
#59954=CARTESIAN_POINT('Ctrl Pts',(-2.56011722181508,-4.01337854620477,
7.27426352484867));
#59955=CARTESIAN_POINT('Ctrl Pts',(-3.49818593160913,-2.86985320272758,
7.22193069373465));
#59956=CARTESIAN_POINT('Ctrl Pts',(-4.15153848320893,-2.0734028007694,7.18548156332043));
#59957=CARTESIAN_POINT('Ctrl Pts',(-4.50676902168756,-1.0324019249735,7.14903243290621));
#59958=CARTESIAN_POINT('Ctrl Pts',(-4.51483246697105,0.00361950456559231,
7.11258330249198));
#59959=CARTESIAN_POINT('Origin',(0.,0.,10.2083368446371));
#59960=CARTESIAN_POINT('',(-5.0799445016814,0.00237344505285342,0.791663155362921));
#59961=CARTESIAN_POINT('',(-5.06551066928822,-0.000578487979983568,0.708336844637072));
#59962=CARTESIAN_POINT('',(-5.0736,1.10600941455115E-13,10.2083368446371));
#59963=CARTESIAN_POINT('',(1.31303618635654,-4.9007502418832,0.));
#59964=CARTESIAN_POINT('Ctrl Pts',(-5.06551066928822,-0.000578487979984235,
0.708336844637072));
#59965=CARTESIAN_POINT('Ctrl Pts',(-5.06491070355288,0.856117806205452,
0.681555887547458));
#59966=CARTESIAN_POINT('Ctrl Pts',(-4.45481520994778,3.38770743142078,0.602442099343825));
#59967=CARTESIAN_POINT('Ctrl Pts',(-0.476761969141785,5.95830217192949,
0.470995480026171));
#59968=CARTESIAN_POINT('Ctrl Pts',(4.70955374493753,3.67573393888292,0.313996986684114));
#59969=CARTESIAN_POINT('Ctrl Pts',(5.49957691269067,-0.955274817987675,
0.183164908899066));
#59970=CARTESIAN_POINT('Ctrl Pts',(3.61105296193539,-3.84612671226304,0.0784992466710263));
#59971=CARTESIAN_POINT('Ctrl Pts',(2.11876087752236,-4.68487601374969,0.0261664155570096));
#59972=CARTESIAN_POINT('Ctrl Pts',(1.31303618635654,-4.90075024188321,0.));
#59973=CARTESIAN_POINT('',(-1.31785621200034,-4.9071451662202,1.75207071073658E-15));
#59974=CARTESIAN_POINT('Origin',(0.,0.,0.));
#59975=CARTESIAN_POINT('Ctrl Pts',(-5.0799445016814,0.00237344505285278,
0.791663155362921));
#59976=CARTESIAN_POINT('Ctrl Pts',(-5.08079896874729,0.146309621287887,
0.787131872330397));
#59977=CARTESIAN_POINT('Ctrl Pts',(-5.01057089916491,1.95175929947146,0.730267758183854));
#59978=CARTESIAN_POINT('Ctrl Pts',(-2.85914249825567,5.24623219278067,0.621070812923292));
#59979=CARTESIAN_POINT('Ctrl Pts',(2.79949684465664,5.27806149196883,0.464072319581235));
#59980=CARTESIAN_POINT('Ctrl Pts',(5.94469888877439,0.578168532022547,0.307073826239177));
#59981=CARTESIAN_POINT('Ctrl Pts',(3.79743415440745,-4.56550609975241,0.152383053045432));
#59982=CARTESIAN_POINT('Ctrl Pts',(0.216274136307286,-5.31234397836678,
0.0500251109657079));
#59983=CARTESIAN_POINT('Ctrl Pts',(-1.31785621200034,-4.9071451662202,1.74231289118421E-15));
#59984=CARTESIAN_POINT('Origin',(0.,0.,10.2083368446371));
#59985=CARTESIAN_POINT('',(-5.06594495534805,0.00113798286105304,1.79166315536292));
#59986=CARTESIAN_POINT('',(-5.0788676065064,-0.0031096904011537,1.70833684463707));
#59987=CARTESIAN_POINT('',(-5.0736,1.10600941455115E-13,10.2083368446371));
#59988=CARTESIAN_POINT('Ctrl Pts',(-5.0788676065064,-0.00310969040115398,
1.70833684463707));
#59989=CARTESIAN_POINT('Ctrl Pts',(-5.06820560204524,1.46267013662722,1.66221954089824));
#59990=CARTESIAN_POINT('Ctrl Pts',(-3.63653147921883,4.60995381904077,1.56376940604539));
#59991=CARTESIAN_POINT('Ctrl Pts',(1.67938795492248,5.73354207176578,1.41298644007852));
#59992=CARTESIAN_POINT('Ctrl Pts',(5.70869045070874,1.76202618095205,1.25598794673646));
#59993=CARTESIAN_POINT('Ctrl Pts',(4.61877209773216,-3.78910839602635,1.0989894533944));
#59994=CARTESIAN_POINT('Ctrl Pts',(-0.612224753988487,-5.94330155793046,
0.941990960052346));
#59995=CARTESIAN_POINT('Ctrl Pts',(-4.49644008704084,-3.30864398166895,
0.811773423799902));
#59996=CARTESIAN_POINT('Ctrl Pts',(-5.06608310024492,-0.817957632158887,
0.733888718661477));
#59997=CARTESIAN_POINT('Ctrl Pts',(-5.06551066928822,-0.000578487979984235,
0.708336844637072));
#59998=CARTESIAN_POINT('Ctrl Pts',(-5.06594495534805,0.00113798286105242,
1.79166315536292));
#59999=CARTESIAN_POINT('Ctrl Pts',(-5.06751102530523,0.764702257078156,
1.76779552568118));
#60000=CARTESIAN_POINT('Ctrl Pts',(-4.54967353500429,3.20046203254748,1.69159506488542));
#60001=CARTESIAN_POINT('Ctrl Pts',(-0.800856996403053,5.92047503909791,
1.56306177297564));
#60002=CARTESIAN_POINT('Ctrl Pts',(4.49633411524324,3.93401017093414,1.40606327963358));
#60003=CARTESIAN_POINT('Ctrl Pts',(5.76163326143087,-1.58003046734643,1.24906478629152));
#60004=CARTESIAN_POINT('Ctrl Pts',(1.86064021890344,-5.67731097226746,1.09206629294947));
#60005=CARTESIAN_POINT('Ctrl Pts',(-3.54825609197855,-4.71238753324782,
0.939599082639932));
#60006=CARTESIAN_POINT('Ctrl Pts',(-5.07093053185417,-1.51604242073639,
0.839464703444417));
#60007=CARTESIAN_POINT('Ctrl Pts',(-5.0799445016814,0.00237344505285278,
0.791663155362921));
#60008=CARTESIAN_POINT('Origin',(0.,0.,10.2083368446371));
#60009=CARTESIAN_POINT('',(-5.07643096335186,-0.00399326016102722,2.79166315536292));
#60010=CARTESIAN_POINT('',(-5.07274549324388,0.00436695056987321,2.70833684463708));
#60011=CARTESIAN_POINT('',(-5.0736,1.10600941455115E-13,10.2083368446371));
#60012=CARTESIAN_POINT('Ctrl Pts',(-5.07274549324388,0.00436695056987284,
2.70833684463708));
#60013=CARTESIAN_POINT('Ctrl Pts',(-5.07638654156454,0.422701167110148,
2.69521602536304));
#60014=CARTESIAN_POINT('Ctrl Pts',(-4.83926758888069,2.50550600890858,2.62976237497499));
#60015=CARTESIAN_POINT('Ctrl Pts',(-1.97561166336026,5.63828895889383,2.51197589347292));
#60016=CARTESIAN_POINT('Ctrl Pts',(3.6128915810316,4.75818989009414,2.35497740013087));
#60017=CARTESIAN_POINT('Ctrl Pts',(5.96174508817349,-0.388546134793637,
2.19797890678881));
#60018=CARTESIAN_POINT('Ctrl Pts',(2.96474106500057,-5.18686823314646,2.04098041344675));
#60019=CARTESIAN_POINT('Ctrl Pts',(-2.69071315072611,-5.33417912211988,
1.88398192010469));
#60020=CARTESIAN_POINT('Ctrl Pts',(-4.98091385691211,-2.06009093973243,
1.77310073050147));
#60021=CARTESIAN_POINT('Ctrl Pts',(-5.08030459382418,-0.200662320374615,
1.71455237201226));
#60022=CARTESIAN_POINT('Ctrl Pts',(-5.0788676065064,-0.00310969040115398,
1.70833684463707));
#60023=CARTESIAN_POINT('Ctrl Pts',(-5.07643096335186,-0.00399326016102722,
2.79166315536292));
#60024=CARTESIAN_POINT('Ctrl Pts',(-5.06457082001664,1.37091447103077,2.74845917903196));
#60025=CARTESIAN_POINT('Ctrl Pts',(-3.7827320999117,4.43074150154599,2.65292237158698));
#60026=CARTESIAN_POINT('Ctrl Pts',(1.36220151697138,5.81702256793933,2.50505273302799));
#60027=CARTESIAN_POINT('Ctrl Pts',(5.60328669734595,2.07280630409542,2.34805423968593));
#60028=CARTESIAN_POINT('Ctrl Pts',(4.81994564291905,-3.53007932713903,2.19105574634387));
#60029=CARTESIAN_POINT('Ctrl Pts',(-0.285401937658034,-5.96757024490932,
2.03405725300181));
#60030=CARTESIAN_POINT('Ctrl Pts',(-4.39760317314566,-3.49692096558582,
1.90092638934149));
#60031=CARTESIAN_POINT('Ctrl Pts',(-5.0640772165997,-0.90951008575328,1.8201283567952));
#60032=CARTESIAN_POINT('Ctrl Pts',(-5.06594495534805,0.00113798286105242,
1.79166315536292));
#60033=CARTESIAN_POINT('Origin',(0.,0.,10.2083368446371));
#60034=CARTESIAN_POINT('',(-5.07544700173093,0.00419220993169878,3.79166315536292));
#60035=CARTESIAN_POINT('',(-5.06752990436066,-0.00289155559083432,3.70833684463708));
#60036=CARTESIAN_POINT('',(-5.0736,1.10600941455115E-13,10.2083368446371));
#60037=CARTESIAN_POINT('Ctrl Pts',(-5.06752990436066,-0.00289155559083445,
3.70833684463708));
#60038=CARTESIAN_POINT('Ctrl Pts',(-5.06201314247005,1.03465176096834,3.67587967871383));
#60039=CARTESIAN_POINT('Ctrl Pts',(-4.25079971500112,3.75301601020252,3.59108968167655));
#60040=CARTESIAN_POINT('Ctrl Pts',(0.164021032340792,5.97213939901987,3.45396685352527));
#60041=CARTESIAN_POINT('Ctrl Pts',(5.07168429591276,3.15774768001703,3.29696836018321));
#60042=CARTESIAN_POINT('Ctrl Pts',(5.43160651478565,-2.48817267483047,3.13996986684115));
#60043=CARTESIAN_POINT('Ctrl Pts',(0.921047975843499,-5.90296718493849,
2.9829713734991));
#60044=CARTESIAN_POINT('Ctrl Pts',(-3.96942410407231,-4.18159504957827,
2.83909369943107));
#60045=CARTESIAN_POINT('Ctrl Pts',(-5.06186409728241,-1.24583899384963,
2.74754885647706));
#60046=CARTESIAN_POINT('Ctrl Pts',(-5.07274549324388,0.00436695056987284,
2.70833684463708));
#60047=CARTESIAN_POINT('Ctrl Pts',(-5.07544700173093,0.00419220993169878,
3.79166315536292));
#60048=CARTESIAN_POINT('Ctrl Pts',(-5.07831876722643,0.329194847520769,
3.78145566349676));
#60049=CARTESIAN_POINT('Ctrl Pts',(-4.90302280847942,2.31737130051307,3.71891534051658));
#60050=CARTESIAN_POINT('Ctrl Pts',(-2.2821043825461,5.52135344516299,3.60404218642239));
#60051=CARTESIAN_POINT('Ctrl Pts',(3.34628151701835,4.94931755856517,3.44704369308033));
#60052=CARTESIAN_POINT('Ctrl Pts',(5.9740820006751,-0.0607341045204584,
3.29004519973827));
#60053=CARTESIAN_POINT('Ctrl Pts',(3.24496813195078,-5.01632594473331,3.13304670639622));
#60054=CARTESIAN_POINT('Ctrl Pts',(-2.39388416789017,-5.47381611497205,
2.97604821305415));
#60055=CARTESIAN_POINT('Ctrl Pts',(-4.9251294092353,-2.24779066275208,2.86225369604306));
#60056=CARTESIAN_POINT('Ctrl Pts',(-5.0789369717198,-0.294506636106011,
2.80079201014598));
#60057=CARTESIAN_POINT('Ctrl Pts',(-5.07643096335186,-0.00399326016102722,
2.79166315536292));
#60058=CARTESIAN_POINT('Origin',(0.,0.,10.2083368446371));
#60059=CARTESIAN_POINT('',(-5.06623538659821,-0.00165077865025204,4.79166315536292));
#60060=CARTESIAN_POINT('',(-5.08150150384863,-0.000304682560140652,4.70833684463708));
#60061=CARTESIAN_POINT('',(-5.0736,1.10600941455115E-13,10.2083368446371));
#60062=CARTESIAN_POINT('Ctrl Pts',(-5.08150150384863,-0.000304682560140828,
4.70833684463708));
#60063=CARTESIAN_POINT('Ctrl Pts',(-5.08004199361202,1.64362562632391,4.65654333206461));
#60064=CARTESIAN_POINT('Ctrl Pts',(-3.32694734261784,4.95128314317388,4.55241698837811));
#60065=CARTESIAN_POINT('Ctrl Pts',(2.28210462993784,5.52135404368456,4.39595781357762));
#60066=CARTESIAN_POINT('Ctrl Pts',(5.86414511529741,1.14243341683897,4.23895932023555));
#60067=CARTESIAN_POINT('Ctrl Pts',(4.18785084798745,-4.2608986517151,4.0819608268935));
#60068=CARTESIAN_POINT('Ctrl Pts',(-1.24365772802729,-5.8435149929827,3.92496233355144));
#60069=CARTESIAN_POINT('Ctrl Pts',(-4.66764902476596,-2.94237266391977,
3.80042100613263));
#60070=CARTESIAN_POINT('Ctrl Pts',(-5.07090818182747,-0.638247816504467,
3.72821250982785));
#60071=CARTESIAN_POINT('Ctrl Pts',(-5.06752990436066,-0.00289155559083445,
3.70833684463708));
#60072=CARTESIAN_POINT('Ctrl Pts',(-5.06623538659821,-0.00165077865025218,
4.79166315536292));
#60073=CARTESIAN_POINT('Ctrl Pts',(-5.06341382264369,0.943369534950495,
4.76211931684755));
#60074=CARTESIAN_POINT('Ctrl Pts',(-4.35931582912874,3.56626810599387,4.68024264721815));
#60075=CARTESIAN_POINT('Ctrl Pts',(-0.164021014606317,5.97213875156532,
4.54603314647473));
#60076=CARTESIAN_POINT('Ctrl Pts',(4.89071815558305,3.43135837605058,4.38903465313268));
#60077=CARTESIAN_POINT('Ctrl Pts',(5.55998718173337,-2.18629522837624,4.23203615979062));
#60078=CARTESIAN_POINT('Ctrl Pts',(1.24365759322077,-5.84351435953346,4.07503766644856));
#60079=CARTESIAN_POINT('Ctrl Pts',(-3.83471277836695,-4.36379434722342,
3.92824666497267));
#60080=CARTESIAN_POINT('Ctrl Pts',(-5.06359550115425,-1.33706248264138,
3.83378849461079));
#60081=CARTESIAN_POINT('Ctrl Pts',(-5.07544700173093,0.00419220993169878,
3.79166315536292));
#60082=CARTESIAN_POINT('Origin',(0.,0.,10.2083368446371));
#60083=CARTESIAN_POINT('',(-5.08061550220448,-0.00187835596255306,5.79166315536292));
#60084=CARTESIAN_POINT('',(-5.06818254924878,0.00327741817492065,5.70833684463708));
#60085=CARTESIAN_POINT('',(-5.0736,1.10600941455115E-13,10.2083368446371));
#60086=CARTESIAN_POINT('Ctrl Pts',(-5.06818254924878,0.00327741817492046,
5.70833684463708));
#60087=CARTESIAN_POINT('Ctrl Pts',(-5.07183456953104,0.603958443996534,
5.68953981652941));
#60088=CARTESIAN_POINT('Ctrl Pts',(-4.69736642816282,2.87259326592426,5.61840995730772));
#60089=CARTESIAN_POINT('Ctrl Pts',(-1.36220166545199,5.81702319809857,5.49494726697201));
#60090=CARTESIAN_POINT('Ctrl Pts',(4.10035928902097,4.34515876133492,5.33794877362997));
#60091=CARTESIAN_POINT('Ctrl Pts',(5.88615929841981,-1.02297668832719,5.1809502802879));
#60092=CARTESIAN_POINT('Ctrl Pts',(2.3938844275315,-5.47381670826519,5.02395178694585));
#60093=CARTESIAN_POINT('Ctrl Pts',(-3.24496848378481,-5.01632648853908,
4.86695329360378));
#60094=CARTESIAN_POINT('Ctrl Pts',(-5.07375293308448,-1.69557487064781,
4.7617483128342));
#60095=CARTESIAN_POINT('Ctrl Pts',(-5.08151670152288,-0.0174226970094883,
4.70887616317863));
#60096=CARTESIAN_POINT('Ctrl Pts',(-5.08150150384863,-0.000304682560140828,
4.70833684463708));
#60097=CARTESIAN_POINT('Ctrl Pts',(-5.08061550220448,-0.00187835596255308,
5.79166315536293));
#60098=CARTESIAN_POINT('Ctrl Pts',(-5.07313315332044,1.5503069404754,5.74278297019833));
#60099=CARTESIAN_POINT('Ctrl Pts',(-3.48999114796195,4.77754415127511,5.64156995391971));
#60100=CARTESIAN_POINT('Ctrl Pts',(1.97561144788205,5.63828834519714,5.48802410652708));
#60101=CARTESIAN_POINT('Ctrl Pts',(5.79259970947732,1.46257867915377,5.33102561318502));
#60102=CARTESIAN_POINT('Ctrl Pts',(4.41540665009831,-4.0246153410012,5.17402711984296));
#60103=CARTESIAN_POINT('Ctrl Pts',(-0.92104787574744,-5.90296654461282,
5.01702862650091));
#60104=CARTESIAN_POINT('Ctrl Pts',(-4.58281307585404,-3.13076536575022,
4.88957397167423));
#60105=CARTESIAN_POINT('Ctrl Pts',(-5.0684118336446,-0.730603481292581,
4.81445214796157));
#60106=CARTESIAN_POINT('Ctrl Pts',(-5.06623538659821,-0.00165077865025218,
4.79166315536292));
#60107=CARTESIAN_POINT('Origin',(0.,0.,10.2083368446371));
#60108=CARTESIAN_POINT('',(-5.07032350272244,0.00406483722298734,6.79166315536293));
#60109=CARTESIAN_POINT('',(-5.07176207912418,-0.00429478512726797,6.70833684463708));
#60110=CARTESIAN_POINT('',(-5.0736,1.10600941455115E-13,10.2083368446371));
#60111=CARTESIAN_POINT('Ctrl Pts',(-5.07176207912418,-0.00429478512726802,
6.70833684463708));
#60112=CARTESIAN_POINT('Ctrl Pts',(-5.06152064599786,1.21211560888524,6.67020346988019));
#60113=CARTESIAN_POINT('Ctrl Pts',(-4.01723926286446,4.11367300543969,6.57973726400929));
#60114=CARTESIAN_POINT('Ctrl Pts',(0.800857062853464,5.92047566764934,6.43693822702436));
#60115=CARTESIAN_POINT('Ctrl Pts',(5.37989341709942,2.59808361512381,6.27993973368231));
#60116=CARTESIAN_POINT('Ctrl Pts',(5.13483694964473,-3.0539846259906,6.12294124034024));
#60117=CARTESIAN_POINT('Ctrl Pts',(0.285401972927619,-5.96757088942664,
5.96594274699819));
#60118=CARTESIAN_POINT('Ctrl Pts',(-4.20869589117159,-3.8219142963774,5.8277412817638));
#60119=CARTESIAN_POINT('Ctrl Pts',(-5.06166697497504,-1.0683984039935,5.74187264764343));
#60120=CARTESIAN_POINT('Ctrl Pts',(-5.06818254924878,0.00327741817492046,
5.70833684463708));
#60121=CARTESIAN_POINT('Ctrl Pts',(-5.07032350272244,0.00406483722298713,
6.79166315536293));
#60122=CARTESIAN_POINT('Ctrl Pts',(-5.07426970367213,0.511087407033013,
6.77577945466313));
#60123=CARTESIAN_POINT('Ctrl Pts',(-4.77323782375589,2.68406204063008,6.70756292284932));
#60124=CARTESIAN_POINT('Ctrl Pts',(-1.67938775292856,5.73354154736347,6.58701355992148));
#60125=CARTESIAN_POINT('Ctrl Pts',(3.85566217988192,4.56363706615652,6.43001506657943));
#60126=CARTESIAN_POINT('Ctrl Pts',(5.93344523009267,-0.69834389981148,6.27301657323736));
#60127=CARTESIAN_POINT('Ctrl Pts',(2.69071284975304,-5.33417856632519,6.11601807989532));
#60128=CARTESIAN_POINT('Ctrl Pts',(-2.96474073765194,-5.18686765769478,
5.95901958655325));
#60129=CARTESIAN_POINT('Ctrl Pts',(-5.0286520759667,-1.88246391579033,5.85090127837579));
#60130=CARTESIAN_POINT('Ctrl Pts',(-5.08114401701022,-0.111516776080137,
5.79511580131235));
#60131=CARTESIAN_POINT('Ctrl Pts',(-5.08061550220448,-0.00187835596255308,
5.79166315536293));
#60132=CARTESIAN_POINT('Origin',(0.,0.,10.2083368446371));
#60133=CARTESIAN_POINT('',(-5.0667809979009,-0.000656412822606089,7.79166315536293));
#60134=CARTESIAN_POINT('',(-5.07934275226421,0.00276793540382957,7.70833684463708));
#60135=CARTESIAN_POINT('',(-5.0736,1.10600941455115E-13,10.2083368446371));
#60136=CARTESIAN_POINT('',(-1.31303618635646,-4.90075024188322,8.));
#60137=CARTESIAN_POINT('Ctrl Pts',(-1.31303618635644,-4.90075024188323,
8.));
#60138=CARTESIAN_POINT('Ctrl Pts',(-2.11876087752226,-4.68487601374973,
7.97383358444299));
#60139=CARTESIAN_POINT('Ctrl Pts',(-3.61103600209076,-3.84612122823184,
7.92150075332897));
#60140=CARTESIAN_POINT('Ctrl Pts',(-4.8640953672922,-1.92805050100101,7.85205513844995));
#60141=CARTESIAN_POINT('Ctrl Pts',(-5.07037793642002,-0.54712311490011,
7.80877593912793));
#60142=CARTESIAN_POINT('Ctrl Pts',(-5.0667809979009,-0.000656412822605951,
7.79166315536293));
#60143=CARTESIAN_POINT('',(1.31785785677863,-4.90714579947409,8.00000000000001));
#60144=CARTESIAN_POINT('Origin',(0.,0.,8.));
#60145=CARTESIAN_POINT('Ctrl Pts',(1.31785785677863,-4.90714579947409,8.00000000000001));
#60146=CARTESIAN_POINT('Ctrl Pts',(-0.216269591468087,-5.31234554625424,
7.9499748890343));
#60147=CARTESIAN_POINT('Ctrl Pts',(-3.61771514871704,-4.60298607712906,
7.85275383724664));
#60148=CARTESIAN_POINT('Ctrl Pts',(-5.07021586478366,-1.49689387689792,
7.75553278545901));
#60149=CARTESIAN_POINT('Ctrl Pts',(-5.07934275226421,0.00276793540382986,
7.70833684463708));
#60150=CARTESIAN_POINT('Origin',(0.,0.,10.2083368446371));
#60151=CARTESIAN_POINT('Ctrl Pts',(-5.07934275226421,0.00276793540383012,
7.70833684463708));
#60152=CARTESIAN_POINT('Ctrl Pts',(-5.08033613895975,0.165993799129837,
7.70319995434499));
#60153=CARTESIAN_POINT('Ctrl Pts',(-4.99920696262547,1.99102187228673,7.64573023293889));
#60154=CARTESIAN_POINT('Ctrl Pts',(-2.799497488489,5.27806255262917,7.53592768041876));
#60155=CARTESIAN_POINT('Ctrl Pts',(2.8591428156985,5.24623244979999,7.37892918707671));
#60156=CARTESIAN_POINT('Ctrl Pts',(5.95237094349663,0.509586379962791,7.22193069373465));
#60157=CARTESIAN_POINT('Ctrl Pts',(3.70900729550924,-4.68371090122276,7.06493220039259));
#60158=CARTESIAN_POINT('Ctrl Pts',(-1.86064034918539,-5.67731151891722,
6.90793370705054));
#60159=CARTESIAN_POINT('Ctrl Pts',(-4.81412133745352,-2.5752195014975,6.78906858846536));
#60160=CARTESIAN_POINT('Ctrl Pts',(-5.07557560949328,-0.457240961862529,
6.72253630099421));
#60161=CARTESIAN_POINT('Ctrl Pts',(-5.07176207912418,-0.00429478512726802,
6.70833684463708));
#60162=CARTESIAN_POINT('Ctrl Pts',(-5.0667809979009,-0.000656412822605951,
7.79166315536293));
#60163=CARTESIAN_POINT('Ctrl Pts',(-5.05937809100424,1.12403395819613,7.75644310801391));
#60164=CARTESIAN_POINT('Ctrl Pts',(-4.14423912611421,3.92453560182124,7.66889022955088));
#60165=CARTESIAN_POINT('Ctrl Pts',(0.476758320675261,5.95830042580594,7.52900451997384));
#60166=CARTESIAN_POINT('Ctrl Pts',(5.22810884028568,2.88800998678043,7.37200602663177));
#60167=CARTESIAN_POINT('Ctrl Pts',(5.29527916712856,-2.76679132542031,7.21500753328971));
#60168=CARTESIAN_POINT('Ctrl Pts',(0.612224870220684,-5.9433011663707,7.05800903994766));
#60169=CARTESIAN_POINT('Ctrl Pts',(-4.08954628424525,-4.00704976176015,
6.91689424730539));
#60170=CARTESIAN_POINT('Ctrl Pts',(-5.0612679560476,-1.15942546766541,6.82811228577715));
#60171=CARTESIAN_POINT('Ctrl Pts',(-5.07032350272244,0.00406483722298713,
6.79166315536293));
#60172=CARTESIAN_POINT('Ctrl Pts',(3.43378788736183,2.93584158413004,8.));
#60173=CARTESIAN_POINT('Ctrl Pts',(3.91646501574697,2.37129788193754,7.97383358444299));
#60174=CARTESIAN_POINT('Ctrl Pts',(4.58922505888624,1.00348867934585,7.92150075332897));
#60175=CARTESIAN_POINT('Ctrl Pts',(4.5186273771248,-2.07044295135642,7.81683509110093));
#60176=CARTESIAN_POINT('Ctrl Pts',(1.60472354186206,-5.07186039848098,7.68600301331589));
#60177=CARTESIAN_POINT('Ctrl Pts',(-3.35287702678038,-4.13364886539305,
7.52900451997383));
#60178=CARTESIAN_POINT('Ctrl Pts',(-5.29341307506948,0.514825336495039,
7.37200602663177));
#60179=CARTESIAN_POINT('Ctrl Pts',(-2.49279205665034,4.69981218407846,7.21500753328972));
#60180=CARTESIAN_POINT('Ctrl Pts',(2.5459028018807,4.67146930189292,7.05800903994766));
#60181=CARTESIAN_POINT('Ctrl Pts',(5.3002451572812,0.453757463748993,6.90101054660559));
#60182=CARTESIAN_POINT('Ctrl Pts',(3.30265841006127,-4.17057610454098,6.74401205326355));
#60183=CARTESIAN_POINT('Ctrl Pts',(-1.6567935859217,-5.05532050508283,6.58701355992147));
#60184=CARTESIAN_POINT('Ctrl Pts',(-5.13040478426442,-1.40692675790748,
6.43001506657944));
#60185=CARTESIAN_POINT('Ctrl Pts',(-4.00372822142153,3.50301097463029,6.27301657323735));
#60186=CARTESIAN_POINT('Ctrl Pts',(0.713117312304132,5.27184424225852,6.11601807989532));
#60187=CARTESIAN_POINT('Ctrl Pts',(4.79048673232043,2.31344454671744,5.95901958655324));
#60188=CARTESIAN_POINT('Ctrl Pts',(4.57227799378301,-2.71939826633338,5.8020210932112));
#60189=CARTESIAN_POINT('Ctrl Pts',(0.254134098705802,-5.31377983792714,
5.64502259986913));
#60190=CARTESIAN_POINT('Ctrl Pts',(-4.2918858010234,-3.14333365162852,5.48802410652709));
#60191=CARTESIAN_POINT('Ctrl Pts',(-4.98940618387219,1.8457154089275,5.33102561318501));
#60192=CARTESIAN_POINT('Ctrl Pts',(-1.21296250672023,5.17972574763675,5.17402711984298));
#60193=CARTESIAN_POINT('Ctrl Pts',(3.65113492943364,3.86911482852823,5.0170286265009));
#60194=CARTESIAN_POINT('Ctrl Pts',(5.24128748234707,-0.910902107712505,
4.86003013315885));
#60195=CARTESIAN_POINT('Ctrl Pts',(2.13161687410921,-4.87412003976763,4.70303163981679));
#60196=CARTESIAN_POINT('Ctrl Pts',(-2.88945844521027,-4.46675122075005,
4.54603314647474));
#60197=CARTESIAN_POINT('Ctrl Pts',(-5.31957818590282,-0.0540802448651307,
4.38903465313267));
#60198=CARTESIAN_POINT('Ctrl Pts',(-2.97967221743332,4.40708408702865,4.23203615979062));
#60199=CARTESIAN_POINT('Ctrl Pts',(2.0320833711569,4.91644931229421,4.07503766644856));
#60200=CARTESIAN_POINT('Ctrl Pts',(5.22168511404818,1.01727147763408,3.9180391731065));
#60201=CARTESIAN_POINT('Ctrl Pts',(3.7290411480005,-3.79408603038985,3.76104067976445));
#60202=CARTESIAN_POINT('Ctrl Pts',(-1.10740592494388,-5.20331517256929,
3.60404218642238));
#60203=CARTESIAN_POINT('Ctrl Pts',(-4.95085044410053,-1.94677080151586,
3.44704369308033));
#60204=CARTESIAN_POINT('Ctrl Pts',(-4.35490467170682,3.05542829226346,3.29004519973827));
#60205=CARTESIAN_POINT('Ctrl Pts',(0.146051328220124,5.31784783386984,3.13304670639621));
#60206=CARTESIAN_POINT('Ctrl Pts',(4.51604417531138,2.81179331862917,2.97604821305416));
#60207=CARTESIAN_POINT('Ctrl Pts',(4.83653428180639,-2.21557515407508,2.8190497197121));
#60208=CARTESIAN_POINT('Ctrl Pts',(0.820140431422849,-5.25625394192603,
2.66205122637004));
#60209=CARTESIAN_POINT('Ctrl Pts',(-3.93166697371103,-3.58368967284698,
2.50505273302798));
#60210=CARTESIAN_POINT('Ctrl Pts',(-5.15797858932007,1.30234262409331,2.34805423968593));
#60211=CARTESIAN_POINT('Ctrl Pts',(-1.75916895146362,5.02057315201092,2.19105574634387));
#60212=CARTESIAN_POINT('Ctrl Pts',(3.21707287531645,4.23689537527058,2.03405725300181));
#60213=CARTESIAN_POINT('Ctrl Pts',(5.30859229582462,-0.345978063005356,
1.87705875965975));
#60214=CARTESIAN_POINT('Ctrl Pts',(2.63993199038283,-4.61860886950043,1.7200602663177));
#60215=CARTESIAN_POINT('Ctrl Pts',(-2.39592583898866,-4.74978077281557,
1.56306177297564));
#60216=CARTESIAN_POINT('Ctrl Pts',(-5.28339345476216,-0.621835317076693,
1.40606327963358));
#60217=CARTESIAN_POINT('Ctrl Pts',(-3.43324656738056,4.06365773166108,1.24906478629152));
#60218=CARTESIAN_POINT('Ctrl Pts',(1.4953987175479,5.10539058946701,1.09206629294947));
#60219=CARTESIAN_POINT('Ctrl Pts',(5.08326164531879,1.56898332130955,0.935067799607405));
#60220=CARTESIAN_POINT('Ctrl Pts',(4.1127518220848,-3.37398384897273,0.778069306265351));
#60221=CARTESIAN_POINT('Ctrl Pts',(-0.545151052966628,-5.29216938925817,
0.621070812923291));
#60222=CARTESIAN_POINT('Ctrl Pts',(-4.71514359968435,-2.4636695471729,0.464072319581234));
#60223=CARTESIAN_POINT('Ctrl Pts',(-4.65533046585126,2.57160754473359,0.307073826239176));
#60224=CARTESIAN_POINT('Ctrl Pts',(-0.424529207286798,5.30552657624457,
0.150075332897118));
#60225=CARTESIAN_POINT('Ctrl Pts',(4.1935876756527,3.27303039309136,-0.00692316044493899));
#60226=CARTESIAN_POINT('Ctrl Pts',(4.89705802532881,-0.850617472596149,
-0.137755238229987));
#60227=CARTESIAN_POINT('Ctrl Pts',(3.21543569039412,-3.42475539150235,-0.242420900458027));
#60228=CARTESIAN_POINT('Ctrl Pts',(1.88663512189109,-4.17161357046627,-0.294753731572044));
#60229=CARTESIAN_POINT('Ctrl Pts',(1.16918346556927,-4.36383719750628,-0.320920147129053));
#60230=CARTESIAN_POINT('Ctrl Pts',(3.574615437742,3.05624720968396,8.10697338237635));
#60231=CARTESIAN_POINT('Ctrl Pts',(4.0770882669231,2.46855026993857,8.08080696681934));
#60232=CARTESIAN_POINT('Ctrl Pts',(4.77743974901458,1.04464406144345,8.02847413570532));
#60233=CARTESIAN_POINT('Ctrl Pts',(4.7039466937149,-2.15535658568851,7.92380847347729));
#60234=CARTESIAN_POINT('Ctrl Pts',(1.67053695050899,-5.27986907555073,7.79297639569223));
#60235=CARTESIAN_POINT('Ctrl Pts',(-3.49038623640434,-4.30317932648753,
7.63597790235018));
#60236=CARTESIAN_POINT('Ctrl Pts',(-5.51050813771329,0.535939509353267,
7.47897940900812));
#60237=CARTESIAN_POINT('Ctrl Pts',(-2.59502720059656,4.8925623069287,7.32198091566607));
#60238=CARTESIAN_POINT('Ctrl Pts',(2.65031613981997,4.86305701786194,7.16498242232401));
#60239=CARTESIAN_POINT('Ctrl Pts',(5.51762041935301,0.472367102486928,7.00798392898195));
#60240=CARTESIAN_POINT('Ctrl Pts',(3.43810803854393,-4.34162103676824,6.85098543563989));
#60241=CARTESIAN_POINT('Ctrl Pts',(-1.72474250700959,-5.26265084302763,
6.69398694229783));
#60242=CARTESIAN_POINT('Ctrl Pts',(-5.34081450144173,-1.46462806485474,
6.53698844895577));
#60243=CARTESIAN_POINT('Ctrl Pts',(-4.16793033765764,3.64667752326241,6.37998995561372));
#60244=CARTESIAN_POINT('Ctrl Pts',(0.742363895820577,5.48805471738879,6.22299146227166));
#60245=CARTESIAN_POINT('Ctrl Pts',(4.98695562724675,2.40832423618623,6.0659929689296));
#60246=CARTESIAN_POINT('Ctrl Pts',(4.75979764573692,-2.83092705288579,5.90899447558755));
#60247=CARTESIAN_POINT('Ctrl Pts',(0.264556723446406,-5.53171018842698,
5.75199598224549));
#60248=CARTESIAN_POINT('Ctrl Pts',(-4.4679059233187,-3.27224900479161,5.59499748890343));
#60249=CARTESIAN_POINT('Ctrl Pts',(-5.19403322368223,1.92141244912467,5.43799899556137));
#60250=CARTESIAN_POINT('Ctrl Pts',(-1.26270889296415,5.39215823112403,5.28100050221931));
#60251=CARTESIAN_POINT('Ctrl Pts',(3.80087638262942,4.02779613946379,5.12400200887726));
#60252=CARTESIAN_POINT('Ctrl Pts',(5.45624475437132,-0.948260301250735,
4.96700351553519));
#60253=CARTESIAN_POINT('Ctrl Pts',(2.21903939191664,-5.07401892926682,4.81000502219315));
#60254=CARTESIAN_POINT('Ctrl Pts',(-3.00796179140179,-4.64994297667973,
4.65300652885108));
#60255=CARTESIAN_POINT('Ctrl Pts',(-5.53774634000859,-0.05629820027127,
4.49600803550903));
#60256=CARTESIAN_POINT('Ctrl Pts',(-3.10187543821507,4.58782875637178,4.33900954216697));
#60257=CARTESIAN_POINT('Ctrl Pts',(2.11542379075055,5.11808422275766,4.18201104882491));
#60258=CARTESIAN_POINT('Ctrl Pts',(5.43583844779792,1.05899212403571,4.02501255548285));
#60259=CARTESIAN_POINT('Ctrl Pts',(3.88197771466281,-3.94969023749826,3.8680140621408));
#60260=CARTESIAN_POINT('Ctrl Pts',(-1.15282319263835,-5.4167151127071,3.71101556879874));
#60261=CARTESIAN_POINT('Ctrl Pts',(-5.15389622421624,-2.0266123561262,3.55401707545668));
#60262=CARTESIAN_POINT('Ctrl Pts',(-4.53350934304161,3.18073844416463,3.39701858211462));
#60263=CARTESIAN_POINT('Ctrl Pts',(0.152041229593681,5.53594502225318,3.24002008877256));
#60264=CARTESIAN_POINT('Ctrl Pts',(4.70125754884517,2.92711143909179,3.08302159543051));
#60265=CARTESIAN_POINT('Ctrl Pts',(5.03489169279947,-2.30644099432688,2.92602310208845));
#60266=CARTESIAN_POINT('Ctrl Pts',(0.853776279563064,-5.47182502293018,
2.7690246087464));
#60267=CARTESIAN_POINT('Ctrl Pts',(-4.09291369219827,-3.730665040722,2.61202611540433));
#60268=CARTESIAN_POINT('Ctrl Pts',(-5.36951917175407,1.3557546948219,2.45502762206228));
#60269=CARTESIAN_POINT('Ctrl Pts',(-1.83131652209583,5.22647842097189,2.29802912872022));
#60270=CARTESIAN_POINT('Ctrl Pts',(3.34901244388816,4.41066021354511,2.14103063537816));
#60271=CARTESIAN_POINT('Ctrl Pts',(5.52630989327424,-0.360167420268118,
1.9840321420361));
#60272=CARTESIAN_POINT('Ctrl Pts',(2.74820168192207,-4.80802865738244,1.82703364869405));
#60273=CARTESIAN_POINT('Ctrl Pts',(-2.49418827623448,-4.94458022258368,
1.67003515535199));
#60274=CARTESIAN_POINT('Ctrl Pts',(-5.50007758969876,-0.647338215717022,
1.51303666200993));
#60275=CARTESIAN_POINT('Ctrl Pts',(-3.57405191698147,4.23031769514908,1.35603816866787));
#60276=CARTESIAN_POINT('Ctrl Pts',(1.55672846333943,5.31477441689994,1.19903967532582));
#60277=CARTESIAN_POINT('Ctrl Pts',(5.2917379137821,1.63333094119038,1.04204118198376));
#60278=CARTESIAN_POINT('Ctrl Pts',(4.28142524730059,-3.5123586979906,0.885042688641701));
#60279=CARTESIAN_POINT('Ctrl Pts',(-0.567508953307252,-5.50921344548227,
0.728044195299643));
#60280=CARTESIAN_POINT('Ctrl Pts',(-4.90852249920177,-2.56471030992692,
0.571045701957585));
#60281=CARTESIAN_POINT('Ctrl Pts',(-4.84625629098129,2.67707509338356,0.414047208615528));
#60282=CARTESIAN_POINT('Ctrl Pts',(-0.441940127905122,5.52311844147288,
0.257048715273468));
#60283=CARTESIAN_POINT('Ctrl Pts',(4.3655763654143,3.40726490835521,0.100050221931412));
#60284=CARTESIAN_POINT('Ctrl Pts',(5.09789765444943,-0.885503254393324,
-0.0307818558536364));
#60285=CARTESIAN_POINT('Ctrl Pts',(3.3473081142412,-3.56521249842258,-0.135447518081676));
#60286=CARTESIAN_POINT('Ctrl Pts',(1.96401037376818,-4.34270105156074,-0.187780349195693));
#60287=CARTESIAN_POINT('Ctrl Pts',(1.21713437249836,-4.54280821229859,-0.213946764752702));
#60288=CARTESIAN_POINT('Ctrl Pts',(3.71544298812217,3.17665283523789,8.21394676475271));
#60289=CARTESIAN_POINT('Ctrl Pts',(4.23771151809924,2.5658026579396,8.1877803491957));
#60290=CARTESIAN_POINT('Ctrl Pts',(4.96565443914292,1.08579944354106,8.13544751808168));
#60291=CARTESIAN_POINT('Ctrl Pts',(4.889266010305,-2.24027022002061,8.03078185585363));
#60292=CARTESIAN_POINT('Ctrl Pts',(1.73635035915592,-5.48787775262049,7.89994977806859));
#60293=CARTESIAN_POINT('Ctrl Pts',(-3.62789544602829,-4.472709787582,7.74295128472654));
#60294=CARTESIAN_POINT('Ctrl Pts',(-5.72760320035712,0.557053682211493,
7.58595279138447));
#60295=CARTESIAN_POINT('Ctrl Pts',(-2.69726234454278,5.08531242977894,7.42895429804241));
#60296=CARTESIAN_POINT('Ctrl Pts',(2.75472947775923,5.05464473383097,7.27195580470038));
#60297=CARTESIAN_POINT('Ctrl Pts',(5.73499568142482,0.490976741224864,7.11495731135828));
#60298=CARTESIAN_POINT('Ctrl Pts',(3.57355766702658,-4.5126659689955,6.95795881801627));
#60299=CARTESIAN_POINT('Ctrl Pts',(-1.7926914280975,-5.46998118097242,6.80096032467417));
#60300=CARTESIAN_POINT('Ctrl Pts',(-5.55122421861904,-1.522329371802,6.64396183133214));
#60301=CARTESIAN_POINT('Ctrl Pts',(-4.33213245389376,3.79034407189453,6.48696333799006));
#60302=CARTESIAN_POINT('Ctrl Pts',(0.771610479337022,5.70426519251906,6.32996484464802));
#60303=CARTESIAN_POINT('Ctrl Pts',(5.18342452217309,2.50320392565502,6.17296635130595));
#60304=CARTESIAN_POINT('Ctrl Pts',(4.94731729769082,-2.9424558394382,6.01596785796391));
#60305=CARTESIAN_POINT('Ctrl Pts',(0.274979348187014,-5.7496405389268,5.85896936462183));
#60306=CARTESIAN_POINT('Ctrl Pts',(-4.64392604561401,-3.40116435795471,
5.70197087127979));
#60307=CARTESIAN_POINT('Ctrl Pts',(-5.39866026349227,1.99710948932185,5.54497237793772));
#60308=CARTESIAN_POINT('Ctrl Pts',(-1.31245527920807,5.6045907146113,5.38797388459567));
#60309=CARTESIAN_POINT('Ctrl Pts',(3.95061783582519,4.18647745039935,5.23097539125361));
#60310=CARTESIAN_POINT('Ctrl Pts',(5.67120202639557,-0.985618494788963,
5.07397689791155));
#60311=CARTESIAN_POINT('Ctrl Pts',(2.30646190972407,-5.273917818766,4.9169784045695));
#60312=CARTESIAN_POINT('Ctrl Pts',(-3.1264651375933,-4.83313473260941,4.75997991122743));
#60313=CARTESIAN_POINT('Ctrl Pts',(-5.75591449411437,-0.058516155677411,
4.60298141788538));
#60314=CARTESIAN_POINT('Ctrl Pts',(-3.22407865899683,4.76857342571492,4.44598292454332));
#60315=CARTESIAN_POINT('Ctrl Pts',(2.19876421034419,5.31971913322111,4.28898443120126));
#60316=CARTESIAN_POINT('Ctrl Pts',(5.64999178154766,1.10071277043733,4.1319859378592));
#60317=CARTESIAN_POINT('Ctrl Pts',(4.03491428132513,-4.10529444460668,3.97498744451715));
#60318=CARTESIAN_POINT('Ctrl Pts',(-1.19824046033282,-5.6301150528449,3.81798895117509));
#60319=CARTESIAN_POINT('Ctrl Pts',(-5.35694200433196,-2.10645391073654,
3.66099045783303));
#60320=CARTESIAN_POINT('Ctrl Pts',(-4.7121140143764,3.30604859606581,3.50399196449097));
#60321=CARTESIAN_POINT('Ctrl Pts',(0.158031130967237,5.75404221063653,3.34699347114891));
#60322=CARTESIAN_POINT('Ctrl Pts',(4.88647092237896,3.04242955955441,3.18999497780686));
#60323=CARTESIAN_POINT('Ctrl Pts',(5.23324910379256,-2.39730683457867,3.0329964844648));
#60324=CARTESIAN_POINT('Ctrl Pts',(0.887412127703281,-5.68739610393434,
2.87599799112275));
#60325=CARTESIAN_POINT('Ctrl Pts',(-4.25416041068552,-3.87764040859701,
2.71899949778068));
#60326=CARTESIAN_POINT('Ctrl Pts',(-5.58105975418807,1.40916676555049,2.56200100443863));
#60327=CARTESIAN_POINT('Ctrl Pts',(-1.90346409272805,5.43238368993286,2.40500251109657));
#60328=CARTESIAN_POINT('Ctrl Pts',(3.48095201245988,4.58442505181962,2.24800401775452));
#60329=CARTESIAN_POINT('Ctrl Pts',(5.74402749072386,-0.374356777530876,
2.09100552441245));
#60330=CARTESIAN_POINT('Ctrl Pts',(2.85647137346132,-4.99744844526445,1.9340070310704));
#60331=CARTESIAN_POINT('Ctrl Pts',(-2.5924507134803,-5.13937967235178,1.77700853772834));
#60332=CARTESIAN_POINT('Ctrl Pts',(-5.71676172463537,-0.672841114357358,
1.62001004438628));
#60333=CARTESIAN_POINT('Ctrl Pts',(-3.71485726658238,4.39697765863709,1.46301155104423));
#60334=CARTESIAN_POINT('Ctrl Pts',(1.61805820913096,5.52415824433286,1.30601305770217));
#60335=CARTESIAN_POINT('Ctrl Pts',(5.50021418224542,1.69767856107122,1.14901456436011));
#60336=CARTESIAN_POINT('Ctrl Pts',(4.45009867251637,-3.65073354700848,0.992016071018051));
#60337=CARTESIAN_POINT('Ctrl Pts',(-0.589866853647869,-5.72625750170636,
0.835017577675995));
#60338=CARTESIAN_POINT('Ctrl Pts',(-5.1019013987192,-2.66575107268096,0.678019084333936));
#60339=CARTESIAN_POINT('Ctrl Pts',(-5.0371821161113,2.78254264203352,0.521020590991878));
#60340=CARTESIAN_POINT('Ctrl Pts',(-0.459351048523452,5.74071030670118,
0.36402209764982));
#60341=CARTESIAN_POINT('Ctrl Pts',(4.53756505517591,3.54149942361907,0.207023604307763));
#60342=CARTESIAN_POINT('Ctrl Pts',(5.29873728357006,-0.920389036190499,
0.076191526522715));
#60343=CARTESIAN_POINT('Ctrl Pts',(3.47918053808829,-3.70566960534281,-0.0284741357053249));
#60344=CARTESIAN_POINT('Ctrl Pts',(2.04138562564527,-4.51378853265522,-0.0808069668193416));
#60345=CARTESIAN_POINT('Ctrl Pts',(1.26508527942745,-4.7217792270909,-0.106973382376351));
#60346=CARTESIAN_POINT('Ctrl Pts',(3.85627053850235,3.29705846079181,8.32092014712906));
#60347=CARTESIAN_POINT('Ctrl Pts',(4.39833476927537,2.66305504594064,8.29475373157205));
#60348=CARTESIAN_POINT('Ctrl Pts',(5.15386912927126,1.12695482563867,8.24242090045804));
#60349=CARTESIAN_POINT('Ctrl Pts',(5.0745853268951,-2.3251838543527,8.13775523822997));
#60350=CARTESIAN_POINT('Ctrl Pts',(1.80216376780286,-5.69588642969024,8.00692316044496));
#60351=CARTESIAN_POINT('Ctrl Pts',(-3.76540465565226,-4.64224024867649,
7.84992466710287));
#60352=CARTESIAN_POINT('Ctrl Pts',(-5.94469826300093,0.578167855069724,
7.69292617376083));
#60353=CARTESIAN_POINT('Ctrl Pts',(-2.799497488489,5.27806255262917,7.53592768041876));
#60354=CARTESIAN_POINT('Ctrl Pts',(2.8591428156985,5.24623244979999,7.37892918707671));
#60355=CARTESIAN_POINT('Ctrl Pts',(5.95237094349663,0.509586379962791,7.22193069373465));
#60356=CARTESIAN_POINT('Ctrl Pts',(3.70900729550924,-4.68371090122276,7.06493220039259));
#60357=CARTESIAN_POINT('Ctrl Pts',(-1.86064034918539,-5.67731151891722,
6.90793370705054));
#60358=CARTESIAN_POINT('Ctrl Pts',(-5.76163393579635,-1.58003067874924,
6.75093521370848));
#60359=CARTESIAN_POINT('Ctrl Pts',(-4.49633457012987,3.93401062052664,6.59393672036642));
#60360=CARTESIAN_POINT('Ctrl Pts',(0.800857062853464,5.92047566764934,6.43693822702436));
#60361=CARTESIAN_POINT('Ctrl Pts',(5.37989341709942,2.59808361512381,6.27993973368231));
#60362=CARTESIAN_POINT('Ctrl Pts',(5.13483694964473,-3.0539846259906,6.12294124034024));
#60363=CARTESIAN_POINT('Ctrl Pts',(0.285401972927619,-5.96757088942664,
5.96594274699819));
#60364=CARTESIAN_POINT('Ctrl Pts',(-4.81994616790931,-3.5300797111178,5.80894425365613));
#60365=CARTESIAN_POINT('Ctrl Pts',(-5.6032873033023,2.07280652951902,5.65194576031408));
#60366=CARTESIAN_POINT('Ctrl Pts',(-1.36220166545199,5.81702319809857,5.49494726697201));
#60367=CARTESIAN_POINT('Ctrl Pts',(4.10035928902097,4.34515876133492,5.33794877362997));
#60368=CARTESIAN_POINT('Ctrl Pts',(5.88615929841981,-1.02297668832719,5.1809502802879));
#60369=CARTESIAN_POINT('Ctrl Pts',(2.3938844275315,-5.47381670826519,5.02395178694585));
#60370=CARTESIAN_POINT('Ctrl Pts',(-3.24496848378481,-5.01632648853908,
4.86695329360378));
#60371=CARTESIAN_POINT('Ctrl Pts',(-5.97408264822014,-0.0607341110835563,
4.70995480026174));
#60372=CARTESIAN_POINT('Ctrl Pts',(-3.34628187977858,4.94931809505806,4.55295630691966));
#60373=CARTESIAN_POINT('Ctrl Pts',(2.28210462993784,5.52135404368456,4.39595781357762));
#60374=CARTESIAN_POINT('Ctrl Pts',(5.86414511529741,1.14243341683897,4.23895932023555));
#60375=CARTESIAN_POINT('Ctrl Pts',(4.18785084798745,-4.2608986517151,4.0819608268935));
#60376=CARTESIAN_POINT('Ctrl Pts',(-1.24365772802729,-5.8435149929827,3.92496233355144));
#60377=CARTESIAN_POINT('Ctrl Pts',(-5.55998778444767,-2.18629546534688,
3.76796384020939));
#60378=CARTESIAN_POINT('Ctrl Pts',(-4.89071868571119,3.43135874796699,3.61096534686732));
#60379=CARTESIAN_POINT('Ctrl Pts',(0.164021032340792,5.97213939901987,3.45396685352527));
#60380=CARTESIAN_POINT('Ctrl Pts',(5.07168429591276,3.15774768001703,3.29696836018321));
#60381=CARTESIAN_POINT('Ctrl Pts',(5.43160651478565,-2.48817267483047,3.13996986684115));
#60382=CARTESIAN_POINT('Ctrl Pts',(0.921047975843499,-5.90296718493849,
2.9829713734991));
#60383=CARTESIAN_POINT('Ctrl Pts',(-4.41540712917277,-4.02461577647203,
2.82597288015704));
#60384=CARTESIAN_POINT('Ctrl Pts',(-5.79260033662206,1.46257883627908,2.66897438681498));
#60385=CARTESIAN_POINT('Ctrl Pts',(-1.97561166336026,5.63828895889383,2.51197589347292));
#60386=CARTESIAN_POINT('Ctrl Pts',(3.6128915810316,4.75818989009414,2.35497740013087));
#60387=CARTESIAN_POINT('Ctrl Pts',(5.96174508817349,-0.388546134793637,
2.19797890678881));
#60388=CARTESIAN_POINT('Ctrl Pts',(2.96474106500057,-5.18686823314646,2.04098041344675));
#60389=CARTESIAN_POINT('Ctrl Pts',(-2.69071315072611,-5.33417912211988,
1.88398192010469));
#60390=CARTESIAN_POINT('Ctrl Pts',(-5.93344585957197,-0.698344012997689,
1.72698342676263));
#60391=CARTESIAN_POINT('Ctrl Pts',(-3.85566261618328,4.5636376221251,1.56998493342058));
#60392=CARTESIAN_POINT('Ctrl Pts',(1.67938795492248,5.73354207176578,1.41298644007852));
#60393=CARTESIAN_POINT('Ctrl Pts',(5.70869045070874,1.76202618095205,1.25598794673646));
#60394=CARTESIAN_POINT('Ctrl Pts',(4.61877209773216,-3.78910839602635,1.0989894533944));
#60395=CARTESIAN_POINT('Ctrl Pts',(-0.612224753988487,-5.94330155793046,
0.941990960052346));
#60396=CARTESIAN_POINT('Ctrl Pts',(-5.29528029823663,-2.76679183543498,
0.784992466710288));
#60397=CARTESIAN_POINT('Ctrl Pts',(-5.22810794124132,2.88801019068349,0.62799397336823));
#60398=CARTESIAN_POINT('Ctrl Pts',(-0.476761969141785,5.95830217192949,
0.470995480026171));
#60399=CARTESIAN_POINT('Ctrl Pts',(4.70955374493753,3.67573393888292,0.313996986684114));
#60400=CARTESIAN_POINT('Ctrl Pts',(5.49957691269067,-0.955274817987675,
0.183164908899066));
#60401=CARTESIAN_POINT('Ctrl Pts',(3.61105296193539,-3.84612671226304,0.0784992466710263));
#60402=CARTESIAN_POINT('Ctrl Pts',(2.11876087752236,-4.68487601374969,0.0261664155570096));
#60403=CARTESIAN_POINT('Ctrl Pts',(1.31303618635654,-4.90075024188321,0.));
#60404=CARTESIAN_POINT('Ctrl Pts',(1.31303618635654,-4.90075024188321,0.));
#60405=CARTESIAN_POINT('Ctrl Pts',(1.45239813196613,-4.85517621763986,-2.47434559251786E-16));
#60406=CARTESIAN_POINT('Ctrl Pts',(1.58927692318379,-4.80351009978137,-1.74819720228364E-15));
#60407=CARTESIAN_POINT('Ctrl Pts',(1.72341090925204,-4.74604460400692,-1.88737914186277E-15));
#60408=CARTESIAN_POINT('Ctrl Pts',(1.85925417986306,-4.68784681892573,-2.02833469262672E-15));
#60409=CARTESIAN_POINT('Ctrl Pts',(1.99228283138741,-4.62370052461763,2.98138735348004E-16));
#60410=CARTESIAN_POINT('Ctrl Pts',(2.12220346118141,-4.55386096654418,1.11022302462516E-16));
#60411=CARTESIAN_POINT('Ctrl Pts',(2.25247560296862,-4.48383245124121,-7.66003908251115E-17));
#60412=CARTESIAN_POINT('Ctrl Pts',(2.37962344910693,-4.40807936214696,-4.32517766211178E-16));
#60413=CARTESIAN_POINT('Ctrl Pts',(2.50332095055395,-4.32681677710386,-4.44089209850063E-16));
#60414=CARTESIAN_POINT('Ctrl Pts',(2.62609735089877,-4.24615930579203,-4.55574487888469E-16));
#60415=CARTESIAN_POINT('Ctrl Pts',(2.74547509807873,-4.16007358686041,1.08564249317406E-16));
#60416=CARTESIAN_POINT('Ctrl Pts',(2.86109774307792,-4.06873562676994,-5.55111512312578E-17));
#60417=CARTESIAN_POINT('Ctrl Pts',(2.90211866182286,-4.03633049506564,-1.13722271327984E-16));
#60418=CARTESIAN_POINT('Ctrl Pts',(2.94266654026491,-4.00326397860027,-2.92134559916121E-15));
#60419=CARTESIAN_POINT('Ctrl Pts',(2.98272412781597,-3.96954306736407,-2.99760216648792E-15));
#60420=CARTESIAN_POINT('Ctrl Pts',(2.99979215651063,-3.95517501587181,-3.03009412016909E-15));
#60421=CARTESIAN_POINT('Ctrl Pts',(3.01677225892353,-3.94068710954429,-2.12566972362838E-15));
#60422=CARTESIAN_POINT('Ctrl Pts',(3.03364729547102,-3.92609378878367,-2.1094237467878E-15));
#60423=CARTESIAN_POINT('Ctrl Pts',(3.14433957478624,-3.83036848867988,-2.00285780240447E-15));
#60424=CARTESIAN_POINT('Ctrl Pts',(3.25067225380611,-3.72997908311154,-3.12896148123733E-15));
#60425=CARTESIAN_POINT('Ctrl Pts',(3.35235973413124,-3.62516300488518,-3.10862446895044E-15));
#60426=CARTESIAN_POINT('Ctrl Pts',(3.36192986162372,-3.61529843523825,-3.10671048898182E-15));
#60427=CARTESIAN_POINT('Ctrl Pts',(3.37145882014037,-3.60539462864919,-2.66105468162811E-15));
#60428=CARTESIAN_POINT('Ctrl Pts',(3.38094635546186,-3.59545176562119,-2.692290834716E-15));
#60429=CARTESIAN_POINT('Ctrl Pts',(3.48180408426425,-3.48975365237926,-3.02597608841997E-15));
#60430=CARTESIAN_POINT('Ctrl Pts',(3.57798405787049,-3.37964444416285,-3.04382432431275E-15));
#60431=CARTESIAN_POINT('Ctrl Pts',(3.66918347167548,-3.26550314479251,-2.94209101525666E-15));
#60432=CARTESIAN_POINT('Ctrl Pts',(3.75971565071324,-3.15219692801907,-2.84110200923889E-15));
#60433=CARTESIAN_POINT('Ctrl Pts',(3.84534031026112,-3.03491668112307,-1.42999735083781E-15));
#60434=CARTESIAN_POINT('Ctrl Pts',(3.92571655230007,-2.91400844798661,-1.72084568816899E-15));
#60435=CARTESIAN_POINT('Ctrl Pts',(3.99657720672258,-2.80741430638731,-1.97726105417974E-15));
#60436=CARTESIAN_POINT('Ctrl Pts',(4.06335815473368,-2.69799970084542,-4.7182430533371E-15));
#60437=CARTESIAN_POINT('Ctrl Pts',(4.12579259176727,-2.58599222827228,-4.96824803519758E-15));
#60438=CARTESIAN_POINT('Ctrl Pts',(4.14218217787996,-2.55658928649489,-5.03387653084013E-15));
#60439=CARTESIAN_POINT('Ctrl Pts',(4.15827206325859,-2.52700763769101,-2.22246092678142E-15));
#60440=CARTESIAN_POINT('Ctrl Pts',(4.17405702945515,-2.49725134739943,-2.08166817117217E-15));
#60441=CARTESIAN_POINT('Ctrl Pts',(4.18546582852437,-2.47574458376403,-1.97990829160411E-15));
#60442=CARTESIAN_POINT('Ctrl Pts',(4.1967169159508,-2.45414332829404,-3.10559938199478E-15));
#60443=CARTESIAN_POINT('Ctrl Pts',(4.20779634099434,-2.4324729617879,-3.08086889333481E-15));
#60444=CARTESIAN_POINT('Ctrl Pts',(4.27314972651924,-2.30464757272886,-2.93499298792804E-15));
#60445=CARTESIAN_POINT('Ctrl Pts',(4.3326198595779,-2.17426195525281,-5.03888835755339E-15));
#60446=CARTESIAN_POINT('Ctrl Pts',(4.38592260758549,-2.04167340157391,-4.413136522885E-15));
#60447=CARTESIAN_POINT('Ctrl Pts',(4.43841100193019,-1.9111105215869,-3.79694485758248E-15));
#60448=CARTESIAN_POINT('Ctrl Pts',(4.48491932736646,-1.77841080748911,-3.47246432590996E-15));
#60449=CARTESIAN_POINT('Ctrl Pts',(4.52512906800885,-1.64389810614591,-3.30291349825984E-15));
#60450=CARTESIAN_POINT('Ctrl Pts',(4.53704337373435,-1.60404145892158,-3.25267491516128E-15));
#60451=CARTESIAN_POINT('Ctrl Pts',(4.54840435272953,-1.56402555907027,-1.86047514559207E-15));
#60452=CARTESIAN_POINT('Ctrl Pts',(4.55920284487768,-1.52385866802948,-1.74860126378462E-15));
#60453=CARTESIAN_POINT('Ctrl Pts',(4.59648625924208,-1.38517645000696,-1.33619040184573E-15));
#60454=CARTESIAN_POINT('Ctrl Pts',(4.62706837090021,-1.24469418107576,-3.1405520603229E-15));
#60455=CARTESIAN_POINT('Ctrl Pts',(4.6510479415724,-1.1028549274787,-3.44169137633799E-15));
#60456=CARTESIAN_POINT('Ctrl Pts',(4.66553556506662,-1.0171605782801,-3.62362928879583E-15));
#60457=CARTESIAN_POINT('Ctrl Pts',(4.67761212738266,-0.93097088404131,-3.48256637849421E-15));
#60458=CARTESIAN_POINT('Ctrl Pts',(4.68729033896278,-0.844384764732073,
-3.60822483003176E-15));
#60459=CARTESIAN_POINT('Ctrl Pts',(4.69282045363923,-0.794909594117687,
-3.68002586902689E-15));
#60460=CARTESIAN_POINT('Ctrl Pts',(4.6975673931995,-0.74530501799734,-2.90670583210387E-15));
#60461=CARTESIAN_POINT('Ctrl Pts',(4.70153256693874,-0.695589781678817,
-3.02535774210355E-15));
#60462=CARTESIAN_POINT('Ctrl Pts',(4.70300273002319,-0.67715691846114,-3.06935017962366E-15));
#60463=CARTESIAN_POINT('Ctrl Pts',(4.70436508297707,-0.658712562708346,
-1.39035176949888E-15));
#60464=CARTESIAN_POINT('Ctrl Pts',(4.70561925922056,-0.640267374588028,
-1.41553435639707E-15));
#60465=CARTESIAN_POINT('Ctrl Pts',(4.71515008316959,-0.500097409167311,
-1.60690363448191E-15));
#60466=CARTESIAN_POINT('Ctrl Pts',(4.71845154780466,-0.359714693128242,
-6.98970443009747E-16));
#60467=CARTESIAN_POINT('Ctrl Pts',(4.71567835888356,-0.219533504962576,
-9.0205620750794E-16));
#60468=CARTESIAN_POINT('Ctrl Pts',(4.71285964179518,-0.0770509255950372,
-1.1084760840775E-15));
#60469=CARTESIAN_POINT('Ctrl Pts',(4.70376507114378,0.065224279671225,-2.40577940367026E-15));
#60470=CARTESIAN_POINT('Ctrl Pts',(4.68850374693714,0.206855299208619,-2.26207941267376E-15));
#60471=CARTESIAN_POINT('Ctrl Pts',(4.67332604169022,0.347710302303635,-2.11916677430768E-15));
#60472=CARTESIAN_POINT('Ctrl Pts',(4.65204869880232,0.487928957857132,-3.70693630030531E-15));
#60473=CARTESIAN_POINT('Ctrl Pts',(4.62472984685344,0.627067645312151,-4.06619182768964E-15));
#60474=CARTESIAN_POINT('Ctrl Pts',(4.60512526025429,0.72691651350792,-4.32400120090221E-15));
#60475=CARTESIAN_POINT('Ctrl Pts',(4.58240838869996,0.826208961746935,-2.80327058352682E-15));
#60476=CARTESIAN_POINT('Ctrl Pts',(4.55658611607818,0.924773126569175,-2.94209101525666E-15));
#60477=CARTESIAN_POINT('Ctrl Pts',(4.54451163215688,0.970861688981747,-3.00700339130591E-15));
#60478=CARTESIAN_POINT('Ctrl Pts',(4.53175798542344,1.01679090044476,-4.8702446610021E-15));
#60479=CARTESIAN_POINT('Ctrl Pts',(4.51832500803005,1.062542528366,-4.8988590961585E-15));
#60480=CARTESIAN_POINT('Ctrl Pts',(4.51266846717592,1.08180824622589,-4.91090845176596E-15));
#60481=CARTESIAN_POINT('Ctrl Pts',(4.50689146090876,1.10104246936981,-1.58247074004002E-15));
#60482=CARTESIAN_POINT('Ctrl Pts',(4.50099394804091,1.12024381085806,-1.56819002228303E-15));
#60483=CARTESIAN_POINT('Ctrl Pts',(4.49471177106765,1.14069755603102,-1.55297784754686E-15));
#60484=CARTESIAN_POINT('Ctrl Pts',(4.48829554526876,1.1611051847425,-3.02768046308214E-15));
#60485=CARTESIAN_POINT('Ctrl Pts',(4.48174652480305,1.18146221251882,-3.05311331771918E-15));
#60486=CARTESIAN_POINT('Ctrl Pts',(4.4388367801027,1.31484320732769,-3.21975156617037E-15));
#60487=CARTESIAN_POINT('Ctrl Pts',(4.3902172033679,1.44609540153194,-2.42101694317024E-15));
#60488=CARTESIAN_POINT('Ctrl Pts',(4.33595560037894,1.57478564497199,-2.33146835171283E-15));
#60489=CARTESIAN_POINT('Ctrl Pts',(4.28905400984558,1.68602041819998,-2.25406607942409E-15));
#60490=CARTESIAN_POINT('Ctrl Pts',(4.23793630897375,1.79534112442678,-2.09120843630436E-15));
#60491=CARTESIAN_POINT('Ctrl Pts',(4.18261934387559,1.90245063170277,-1.54737334057131E-15));
#60492=CARTESIAN_POINT('Ctrl Pts',(4.15876651886949,1.94863654101668,-1.31287017598733E-15));
#60493=CARTESIAN_POINT('Ctrl Pts',(4.13413259613109,1.99441106904023,-3.34114378130206E-15));
#60494=CARTESIAN_POINT('Ctrl Pts',(4.1087175751394,2.03974918362091,-3.32373017997156E-15));
#60495=CARTESIAN_POINT('Ctrl Pts',(4.09757084929567,2.05963394128716,-3.31609278159812E-15));
#60496=CARTESIAN_POINT('Ctrl Pts',(4.08627386148571,2.07943474030452,-3.10826804513356E-15));
#60497=CARTESIAN_POINT('Ctrl Pts',(4.07482656400744,2.09914941832117,-3.21964677141295E-15));
#60498=CARTESIAN_POINT('Ctrl Pts',(4.06286705490573,2.11974623356295,-3.33600916115644E-15));
#60499=CARTESIAN_POINT('Ctrl Pts',(4.05074796307183,2.14024130439856,-5.56609850953026E-16));
#60500=CARTESIAN_POINT('Ctrl Pts',(4.03847105489573,2.16062996612303,-7.21644966006352E-16));
#60501=CARTESIAN_POINT('Ctrl Pts',(3.96920184151707,2.27566760746066,-1.65281203475204E-15));
#60502=CARTESIAN_POINT('Ctrl Pts',(3.89489673126452,2.38734604756407,-5.44084181235126E-15));
#60503=CARTESIAN_POINT('Ctrl Pts',(3.81559015152877,2.49525778868992,-3.92741394961149E-15));
#60504=CARTESIAN_POINT('Ctrl Pts',(3.73966418517796,2.5985695599563,-2.47849920176032E-15));
#60505=CARTESIAN_POINT('Ctrl Pts',(3.65915364949516,2.69842924853399,9.77632756533034E-16));
#60506=CARTESIAN_POINT('Ctrl Pts',(3.57405694815596,2.79444772885285,1.90646110009851E-15));
#60507=CARTESIAN_POINT('Ctrl Pts',(3.53072890723773,2.84333672899846,2.33391700333807E-15));
#60508=CARTESIAN_POINT('Ctrl Pts',(3.48621138925297,2.89122932971802,2.44271821993007E-16));
#60509=CARTESIAN_POINT('Ctrl Pts',(3.44055068766011,2.93810645203839,2.77555756156289E-16));
#60510=CARTESIAN_POINT('Ctrl Pts',(3.43378788736183,2.93584158413004,8.));
#60511=CARTESIAN_POINT('Ctrl Pts',(3.52723828091404,2.83914431545175,8.));
#60512=CARTESIAN_POINT('Ctrl Pts',(3.61594081851665,2.73846055769803,8.));
#60513=CARTESIAN_POINT('Ctrl Pts',(3.69984090589852,2.63418809372837,8.));
#60514=CARTESIAN_POINT('Ctrl Pts',(3.78516287227981,2.52814849421259,8.));
#60515=CARTESIAN_POINT('Ctrl Pts',(3.86551863442571,2.41839706286655,8.));
#60516=CARTESIAN_POINT('Ctrl Pts',(3.94081955158113,2.30530820215193,8.));
#60517=CARTESIAN_POINT('Ctrl Pts',(4.01714046916727,2.19068747846675,8.));
#60518=CARTESIAN_POINT('Ctrl Pts',(4.08826910733635,2.07263776324572,8.));
#60519=CARTESIAN_POINT('Ctrl Pts',(4.15407500660322,1.95151170764482,8.));
#60520=CARTESIAN_POINT('Ctrl Pts',(4.2198164513151,1.83050429073889,8.));
#60521=CARTESIAN_POINT('Ctrl Pts',(4.28024594506117,1.70642592249187,8.));
#60522=CARTESIAN_POINT('Ctrl Pts',(4.33518967485951,1.57960030623271,8.));
#60523=CARTESIAN_POINT('Ctrl Pts',(4.35307625782352,1.53831303076909,8.));
#60524=CARTESIAN_POINT('Ctrl Pts',(4.37038109771682,1.49673442540794,8.));
#60525=CARTESIAN_POINT('Ctrl Pts',(4.3870970941841,1.45487519313349,8.));
#60526=CARTESIAN_POINT('Ctrl Pts',(4.39376575085273,1.43817592851012,8.));
#60527=CARTESIAN_POINT('Ctrl Pts',(4.40033736934907,1.42144028204873,8.));
#60528=CARTESIAN_POINT('Ctrl Pts',(4.40681102745828,1.40467100393547,8.));
#60529=CARTESIAN_POINT('Ctrl Pts',(4.45934053196233,1.26859927210788,8.));
#60530=CARTESIAN_POINT('Ctrl Pts',(4.50544025366947,1.13027539792009,8.));
#60531=CARTESIAN_POINT('Ctrl Pts',(4.54499873531868,0.990127463611741,8.));
#60532=CARTESIAN_POINT('Ctrl Pts',(4.58299050839006,0.855530070216331,8.));
#60533=CARTESIAN_POINT('Ctrl Pts',(4.61494911931547,0.719249512352558,8.));
#60534=CARTESIAN_POINT('Ctrl Pts',(4.64085249468742,0.581767615475945,8.));
#60535=CARTESIAN_POINT('Ctrl Pts',(4.66691769963291,0.443426809811538,8.));
#60536=CARTESIAN_POINT('Ctrl Pts',(4.68685201899535,0.303868786404607,8.));
#60537=CARTESIAN_POINT('Ctrl Pts',(4.70058414747143,0.163565049614876,8.));
#60538=CARTESIAN_POINT('Ctrl Pts',(4.71271762019861,0.0395950789853681,
8.));
#60539=CARTESIAN_POINT('Ctrl Pts',(4.72000832561645,-0.0849577470138994,
8.));
#60540=CARTESIAN_POINT('Ctrl Pts',(4.7223733384523,-0.209772800136726,8.));
#60541=CARTESIAN_POINT('Ctrl Pts',(4.72292943816615,-0.239121315406544,
8.));
#60542=CARTESIAN_POINT('Ctrl Pts',(4.7232130590816,-0.268484329285888,8.));
#60543=CARTESIAN_POINT('Ctrl Pts',(4.72322285747563,-0.297857662780827,
8.));
#60544=CARTESIAN_POINT('Ctrl Pts',(4.72323033779459,-0.320281939952091,
8.));
#60545=CARTESIAN_POINT('Ctrl Pts',(4.72307812055779,-0.342714494826838,
8.));
#60546=CARTESIAN_POINT('Ctrl Pts',(4.72276611337907,-0.365130653249834,
8.));
#60547=CARTESIAN_POINT('Ctrl Pts',(4.72077139214363,-0.508441417465993,
8.));
#60548=CARTESIAN_POINT('Ctrl Pts',(4.71225120797944,-0.651280085007766,
8.));
#60549=CARTESIAN_POINT('Ctrl Pts',(4.69718547532262,-0.793154607131843,
8.));
#60550=CARTESIAN_POINT('Ctrl Pts',(4.68212772666397,-0.934953943670782,
8.));
#60551=CARTESIAN_POINT('Ctrl Pts',(4.66053153776914,-1.07579102267899,8.));
#60552=CARTESIAN_POINT('Ctrl Pts',(4.63232650453452,-1.21518583219434,8.));
#60553=CARTESIAN_POINT('Ctrl Pts',(4.62517817164043,-1.25051429622537,8.));
#60554=CARTESIAN_POINT('Ctrl Pts',(4.6176050749471,-1.28575013896589,8.));
#60555=CARTESIAN_POINT('Ctrl Pts',(4.60960553319191,-1.32088555816255,8.));
#60556=CARTESIAN_POINT('Ctrl Pts',(4.57835655312357,-1.45813667176012,8.));
#60557=CARTESIAN_POINT('Ctrl Pts',(4.54060431924761,-1.59385616146054,8.));
#60558=CARTESIAN_POINT('Ctrl Pts',(4.49667031501799,-1.72776662727194,8.));
#60559=CARTESIAN_POINT('Ctrl Pts',(4.46792000249182,-1.81539733178229,8.));
#60560=CARTESIAN_POINT('Ctrl Pts',(4.43652132007444,-1.90225320075805,8.));
#60561=CARTESIAN_POINT('Ctrl Pts',(4.4025528899726,-1.98825323145006,8.));
#60562=CARTESIAN_POINT('Ctrl Pts',(4.39064088821649,-2.01841160243036,8.));
#60563=CARTESIAN_POINT('Ctrl Pts',(4.37841279355623,-2.04846469658551,8.));
#60564=CARTESIAN_POINT('Ctrl Pts',(4.36587175340618,-2.07840891566329,8.));
#60565=CARTESIAN_POINT('Ctrl Pts',(4.35885849939885,-2.09515444968045,8.));
#60566=CARTESIAN_POINT('Ctrl Pts',(4.35174737519127,-2.11186593393486,8.));
#60567=CARTESIAN_POINT('Ctrl Pts',(4.34453891478344,-2.12854273059161,8.));
#60568=CARTESIAN_POINT('Ctrl Pts',(4.33664233992457,-2.14681148227446,8.));
#60569=CARTESIAN_POINT('Ctrl Pts',(4.32863248368416,-2.16503040522278,8.));
#60570=CARTESIAN_POINT('Ctrl Pts',(4.32051229345552,-2.18319454758947,8.));
#60571=CARTESIAN_POINT('Ctrl Pts',(4.26271734267779,-2.31247670532764,8.));
#60572=CARTESIAN_POINT('Ctrl Pts',(4.19930769062008,-2.43905306787665,8.));
#60573=CARTESIAN_POINT('Ctrl Pts',(4.1306563766664,-2.56266246904431,8.));
#60574=CARTESIAN_POINT('Ctrl Pts',(4.05932719227651,-2.69109348165625,8.));
#60575=CARTESIAN_POINT('Ctrl Pts',(3.98233931388035,-2.81632224208436,8.));
#60576=CARTESIAN_POINT('Ctrl Pts',(3.90005514682149,-2.93804448640157,8.));
#60577=CARTESIAN_POINT('Ctrl Pts',(3.81788412514087,-3.05959935575629,8.));
#60578=CARTESIAN_POINT('Ctrl Pts',(3.73043085662906,-3.17765799919859,8.));
#60579=CARTESIAN_POINT('Ctrl Pts',(3.63800695579095,-3.29189623321801,8.));
#60580=CARTESIAN_POINT('Ctrl Pts',(3.56857767496828,-3.37771254651463,8.));
#60581=CARTESIAN_POINT('Ctrl Pts',(3.49634236728105,-3.46137260211582,8.));
#60582=CARTESIAN_POINT('Ctrl Pts',(3.42141741611953,-3.54272769601374,8.));
#60583=CARTESIAN_POINT('Ctrl Pts',(3.38628453897598,-3.58087571579362,8.));
#60584=CARTESIAN_POINT('Ctrl Pts',(3.35056009922657,-3.61851677693959,8.));
#60585=CARTESIAN_POINT('Ctrl Pts',(3.3142552023334,-3.65563464117867,8.));
#60586=CARTESIAN_POINT('Ctrl Pts',(3.299200603776,-3.67102635395701,8.));
#60587=CARTESIAN_POINT('Ctrl Pts',(3.28404454782071,-3.68632972667595,8.));
#60588=CARTESIAN_POINT('Ctrl Pts',(3.26879310797022,-3.70153828550149,8.));
#60589=CARTESIAN_POINT('Ctrl Pts',(3.16313496534899,-3.80689935915782,8.));
#60590=CARTESIAN_POINT('Ctrl Pts',(3.05310906400962,-3.90750842604698,8.));
#60591=CARTESIAN_POINT('Ctrl Pts',(2.93905349297435,-4.00304219163214,8.));
#60592=CARTESIAN_POINT('Ctrl Pts',(2.83343523748027,-4.09150880111292,8.));
#60593=CARTESIAN_POINT('Ctrl Pts',(2.72436063892977,-4.17562341526862,8.));
#60594=CARTESIAN_POINT('Ctrl Pts',(2.61206707761722,-4.25510461849443,8.));
#60595=CARTESIAN_POINT('Ctrl Pts',(2.56057116079448,-4.29155334611912,8.));
#60596=CARTESIAN_POINT('Ctrl Pts',(2.50839792228814,-4.3270273021059,8.));
#60597=CARTESIAN_POINT('Ctrl Pts',(2.45556847535629,-4.3614972584752,8.));
#60598=CARTESIAN_POINT('Ctrl Pts',(2.42827791858812,-4.37930369703788,8.));
#60599=CARTESIAN_POINT('Ctrl Pts',(2.40081223344856,-4.39684219182932,8.));
#60600=CARTESIAN_POINT('Ctrl Pts',(2.37317422709578,-4.41410855841438,8.));
#60601=CARTESIAN_POINT('Ctrl Pts',(2.35241127848289,-4.42707985155184,8.));
#60602=CARTESIAN_POINT('Ctrl Pts',(2.33155925321721,-4.43989244410762,8.));
#60603=CARTESIAN_POINT('Ctrl Pts',(2.31062069154639,-4.45254421740167,8.));
#60604=CARTESIAN_POINT('Ctrl Pts',(2.18359867140573,-4.52929513408044,8.));
#60605=CARTESIAN_POINT('Ctrl Pts',(2.05338150515115,-4.60013897577206,8.00000000000001));
#60606=CARTESIAN_POINT('Ctrl Pts',(1.9202708514578,-4.66473499429566,8.00000000000001));
#60607=CARTESIAN_POINT('Ctrl Pts',(1.79118849882964,-4.72737615644222,8.00000000000001));
#60608=CARTESIAN_POINT('Ctrl Pts',(1.65938453798209,-4.78414231274042,8.00000000000001));
#60609=CARTESIAN_POINT('Ctrl Pts',(1.52510693593821,-4.83468454964306,8.00000000000001));
#60610=CARTESIAN_POINT('Ctrl Pts',(1.45664940136588,-4.86045204085127,8.00000000000001));
#60611=CARTESIAN_POINT('Ctrl Pts',(1.38754853402863,-4.88460115986285,8.00000000000001));
#60612=CARTESIAN_POINT('Ctrl Pts',(1.31785785677859,-4.9071457994741,8.00000000000001));
#60613=CARTESIAN_POINT('Ctrl Pts',(-4.51611343680291,-0.0038242599945422,
6.38741669750802));
#60614=CARTESIAN_POINT('Ctrl Pts',(-4.51950916701914,-0.407146869176555,
6.40161615386516));
#60615=CARTESIAN_POINT('Ctrl Pts',(-4.46982237313174,-0.809647705501708,
6.41581561022229));
#60616=CARTESIAN_POINT('Ctrl Pts',(-4.36369015740015,-1.19666942701374,
6.43001506657943));
#60617=CARTESIAN_POINT('Ctrl Pts',(-3.97253438481685,-2.62305800696593,
6.48234789769345));
#60618=CARTESIAN_POINT('Ctrl Pts',(-2.81466398536927,-3.83918925602438,
6.53468072880746));
#60619=CARTESIAN_POINT('Ctrl Pts',(-1.40915345298166,-4.2997974804633,6.58701355992148));
#60620=CARTESIAN_POINT('Ctrl Pts',(-0.0036429205940397,-4.76040570490222,
6.6393463910355));
#60621=CARTESIAN_POINT('Ctrl Pts',(1.64950774473362,-4.4654909047216,6.69167922214952));
#60622=CARTESIAN_POINT('Ctrl Pts',(2.8090142019341,-3.54731124324962,6.74401205326355));
#60623=CARTESIAN_POINT('Ctrl Pts',(3.96852065913458,-2.62913158177766,6.79634488437757));
#60624=CARTESIAN_POINT('Ctrl Pts',(4.63438290820789,-1.08768705901433,6.84867771549158));
#60625=CARTESIAN_POINT('Ctrl Pts',(4.50825697351113,0.385987175391315,6.9010105466056));
#60626=CARTESIAN_POINT('Ctrl Pts',(4.38213103881437,1.85966140979697,6.95334337771962));
#60627=CARTESIAN_POINT('Ctrl Pts',(3.46401692034753,3.26556535584495,7.00567620883364));
#60628=CARTESIAN_POINT('Ctrl Pts',(2.16517738469227,3.97324114256653,7.05800903994766));
#60629=CARTESIAN_POINT('Ctrl Pts',(0.866337849037014,4.6809169292881,7.11034187106168));
#60630=CARTESIAN_POINT('Ctrl Pts',(-0.81322710380666,4.69036455668328,7.1626747021757));
#60631=CARTESIAN_POINT('Ctrl Pts',(-2.11977974996502,3.9975905624503,7.21500753328971));
#60632=CARTESIAN_POINT('Ctrl Pts',(-3.42633239612339,3.30481656821732,7.26734036440373));
#60633=CARTESIAN_POINT('Ctrl Pts',(-4.35987273559643,1.90982095235617,7.31967319551775));
#60634=CARTESIAN_POINT('Ctrl Pts',(-4.50322023061811,0.437577444110917,
7.37200602663177));
#60635=CARTESIAN_POINT('Ctrl Pts',(-4.51729094569115,0.293064846108908,
7.37714291692385));
#60636=CARTESIAN_POINT('Ctrl Pts',(-4.52374814565307,0.14780796397411,7.38227980721594));
#60637=CARTESIAN_POINT('Ctrl Pts',(-4.52286359173795,0.00246468782935438,
7.38741669750802));
#60638=CARTESIAN_POINT('Ctrl Pts',(-1.31303618635644,-4.90075024188323,
8.));
#60639=CARTESIAN_POINT('Ctrl Pts',(-2.11876087752226,-4.68487601374973,
7.97383358444299));
#60640=CARTESIAN_POINT('Ctrl Pts',(-3.61103600209076,-3.84612122823184,
7.92150075332897));
#60641=CARTESIAN_POINT('Ctrl Pts',(-5.49959712288033,-0.955281493922513,
7.81683509110094));
#60642=CARTESIAN_POINT('Ctrl Pts',(-4.70954440514987,3.67573693777646,7.68600301331588));
#60643=CARTESIAN_POINT('Ctrl Pts',(0.476758320675261,5.95830042580594,7.52900451997384));
#60644=CARTESIAN_POINT('Ctrl Pts',(5.22810884028568,2.88800998678043,7.37200602663177));
#60645=CARTESIAN_POINT('Ctrl Pts',(5.29527916712856,-2.76679132542031,7.21500753328971));
#60646=CARTESIAN_POINT('Ctrl Pts',(0.612224870220684,-5.9433011663707,7.05800903994766));
#60647=CARTESIAN_POINT('Ctrl Pts',(-4.61877163601819,-3.7891077783966,6.90101054660559));
#60648=CARTESIAN_POINT('Ctrl Pts',(-5.70868984087812,1.76202584286959,6.74401205326355));
#60649=CARTESIAN_POINT('Ctrl Pts',(-1.67938775292856,5.73354154736347,6.58701355992148));
#60650=CARTESIAN_POINT('Ctrl Pts',(3.85566217988192,4.56363706615652,6.43001506657943));
#60651=CARTESIAN_POINT('Ctrl Pts',(5.93344523009267,-0.69834389981148,6.27301657323736));
#60652=CARTESIAN_POINT('Ctrl Pts',(2.69071284975304,-5.33417856632519,6.11601807989532));
#60653=CARTESIAN_POINT('Ctrl Pts',(-2.96474073765194,-5.18686765769478,
5.95901958655325));
#60654=CARTESIAN_POINT('Ctrl Pts',(-5.96174444561926,-0.38854610033802,
5.8020210932112));
#60655=CARTESIAN_POINT('Ctrl Pts',(-3.61289118716291,4.75818937870979,5.64502259986913));
#60656=CARTESIAN_POINT('Ctrl Pts',(1.97561144788205,5.63828834519714,5.48802410652708));
#60657=CARTESIAN_POINT('Ctrl Pts',(5.79259970947732,1.46257867915377,5.33102561318502));
#60658=CARTESIAN_POINT('Ctrl Pts',(4.41540665009831,-4.0246153410012,5.17402711984296));
#60659=CARTESIAN_POINT('Ctrl Pts',(-0.92104787574744,-5.90296654461282,
5.01702862650091));
#60660=CARTESIAN_POINT('Ctrl Pts',(-5.43160592614493,-2.48817240536104,
4.86003013315885));
#60661=CARTESIAN_POINT('Ctrl Pts',(-5.07168374606222,3.15774733785514,4.70303163981679));
#60662=CARTESIAN_POINT('Ctrl Pts',(-0.164021014606317,5.97213875156532,
4.54603314647473));
#60663=CARTESIAN_POINT('Ctrl Pts',(4.89071815558305,3.43135837605058,4.38903465313268));
#60664=CARTESIAN_POINT('Ctrl Pts',(5.55998718173337,-2.18629522837624,4.23203615979062));
#60665=CARTESIAN_POINT('Ctrl Pts',(1.24365759322077,-5.84351435953346,4.07503766644856));
#60666=CARTESIAN_POINT('Ctrl Pts',(-4.1878503940255,-4.26089818984331,3.91803917310651));
#60667=CARTESIAN_POINT('Ctrl Pts',(-5.86414447963045,1.14243329300625,3.76104067976444));
#60668=CARTESIAN_POINT('Ctrl Pts',(-2.2821043825461,5.52135344516299,3.60404218642239));
#60669=CARTESIAN_POINT('Ctrl Pts',(3.34628151701835,4.94931755856517,3.44704369308033));
#60670=CARTESIAN_POINT('Ctrl Pts',(5.9740820006751,-0.0607341045204584,
3.29004519973827));
#60671=CARTESIAN_POINT('Ctrl Pts',(3.24496813195078,-5.01632594473331,3.13304670639622));
#60672=CARTESIAN_POINT('Ctrl Pts',(-2.39388416789017,-5.47381611497205,
2.97604821305415));
#60673=CARTESIAN_POINT('Ctrl Pts',(-5.88615866062065,-1.02297657731424,
2.8190497197121));
#60674=CARTESIAN_POINT('Ctrl Pts',(-4.10035884408111,4.34515829009749,2.66205122637004));
#60675=CARTESIAN_POINT('Ctrl Pts',(1.36220151697138,5.81702256793933,2.50505273302799));
#60676=CARTESIAN_POINT('Ctrl Pts',(5.60328669734595,2.07280630409542,2.34805423968593));
#60677=CARTESIAN_POINT('Ctrl Pts',(4.81994564291905,-3.53007932713903,2.19105574634387));
#60678=CARTESIAN_POINT('Ctrl Pts',(-0.285401937658034,-5.96757024490932,
2.03405725300181));
#60679=CARTESIAN_POINT('Ctrl Pts',(-5.13483640041478,-3.05398429071519,
1.87705875965975));
#60680=CARTESIAN_POINT('Ctrl Pts',(-5.37989282152843,2.59808332599247,1.7200602663177));
#60681=CARTESIAN_POINT('Ctrl Pts',(-0.800856996403053,5.92047503909791,
1.56306177297564));
#60682=CARTESIAN_POINT('Ctrl Pts',(4.49633411524324,3.93401017093414,1.40606327963358));
#60683=CARTESIAN_POINT('Ctrl Pts',(5.76163326143087,-1.58003046734643,1.24906478629152));
#60684=CARTESIAN_POINT('Ctrl Pts',(1.86064021890344,-5.67731097226746,1.09206629294947));
#60685=CARTESIAN_POINT('Ctrl Pts',(-3.70900698411085,-4.68371027734449,
0.935067799607409));
#60686=CARTESIAN_POINT('Ctrl Pts',(-5.9523702132809,0.509586132109229,0.77806930626535));
#60687=CARTESIAN_POINT('Ctrl Pts',(-2.85914249825567,5.24623219278067,0.621070812923292));
#60688=CARTESIAN_POINT('Ctrl Pts',(2.79949684465664,5.27806149196883,0.464072319581235));
#60689=CARTESIAN_POINT('Ctrl Pts',(5.94469888877439,0.578168532022547,0.307073826239177));
#60690=CARTESIAN_POINT('Ctrl Pts',(3.76540065952631,-4.64224087416102,0.150075332897119));
#60691=CARTESIAN_POINT('Ctrl Pts',(-1.80215437063507,-5.69588361575389,
-0.00692316044493745));
#60692=CARTESIAN_POINT('Ctrl Pts',(-5.07460576691081,-2.32518978947096,
-0.137755238229986));
#60693=CARTESIAN_POINT('Ctrl Pts',(-5.15385204348173,1.12695990370127,-0.242420900458024));
#60694=CARTESIAN_POINT('Ctrl Pts',(-4.39833476927544,2.66305504594052,-0.294753731572044));
#60695=CARTESIAN_POINT('Ctrl Pts',(-3.85627053850243,3.2970584607917,-0.320920147129053));
#60696=CARTESIAN_POINT('Ctrl Pts',(-1.26508527942735,-4.72177922709092,
8.10697338237635));
#60697=CARTESIAN_POINT('Ctrl Pts',(-2.04138562564518,-4.51378853265526,
8.08080696681934));
#60698=CARTESIAN_POINT('Ctrl Pts',(-3.47916419760203,-3.70566432158352,
8.02847413570533));
#60699=CARTESIAN_POINT('Ctrl Pts',(-5.29875675570167,-0.920395468326166,
7.92380847347728));
#60700=CARTESIAN_POINT('Ctrl Pts',(-4.53755605646894,3.54150231299569,7.79297639569223));
#60701=CARTESIAN_POINT('Ctrl Pts',(0.459347533295664,5.74070862434451,7.63597790235019));
#60702=CARTESIAN_POINT('Ctrl Pts',(5.03718298232336,2.78254244557681,7.47897940900812));
#60703=CARTESIAN_POINT('Ctrl Pts',(5.10190030891819,-2.66575058129155,7.32198091566607));
#60704=CARTESIAN_POINT('Ctrl Pts',(0.589866965635366,-5.72625712444602,
7.16498242232401));
#60705=CARTESIAN_POINT('Ctrl Pts',(-4.45009822766378,-3.650732951934,7.00798392898195));
#60706=CARTESIAN_POINT('Ctrl Pts',(-5.50021359468528,1.69767823533522,6.8509854356399));
#60707=CARTESIAN_POINT('Ctrl Pts',(-1.61805801451367,5.52415773908126,6.69398694229783));
#60708=CARTESIAN_POINT('Ctrl Pts',(3.71485684621434,4.39697712297199,6.53698844895578));
#60709=CARTESIAN_POINT('Ctrl Pts',(5.71676111814409,-0.672841005304612,
6.37998995561372));
#60710=CARTESIAN_POINT('Ctrl Pts',(2.5924504234985,-5.13937913685421,6.22299146227166));
#60711=CARTESIAN_POINT('Ctrl Pts',(-2.85647105806718,-4.99744789082776,
6.0659929689296));
#60712=CARTESIAN_POINT('Ctrl Pts',(-5.74402687163513,-0.374356744333544,
5.90899447558755));
#60713=CARTESIAN_POINT('Ctrl Pts',(-3.48095163297493,4.58442455911056,5.75199598224549));
#60714=CARTESIAN_POINT('Ctrl Pts',(1.90346388511891,5.43238309864782,5.59499748890343));
#60715=CARTESIAN_POINT('Ctrl Pts',(5.58105914994609,1.40916661416325,5.43799899556138));
#60716=CARTESIAN_POINT('Ctrl Pts',(4.25415994910644,-3.8776399890292,5.28100050221931));
#60717=CARTESIAN_POINT('Ctrl Pts',(-0.887412031262641,-5.68739548699278,
5.12400200887726));
#60718=CARTESIAN_POINT('Ctrl Pts',(-5.23324853664848,-2.39730657495003,
4.9670035155352));
#60719=CARTESIAN_POINT('Ctrl Pts',(-4.88647039260848,3.04242922988797,4.81000502219315));
#60720=CARTESIAN_POINT('Ctrl Pts',(-0.15803111388041,5.75404158682643,4.65300652885108));
#60721=CARTESIAN_POINT('Ctrl Pts',(4.71211350360807,3.30604823773145,4.49600803550903));
#60722=CARTESIAN_POINT('Ctrl Pts',(5.35694142362824,-2.10645368241985,4.33900954216697));
#60723=CARTESIAN_POINT('Ctrl Pts',(1.19824033044931,-5.63011444252866,4.18201104882491));
#60724=CARTESIAN_POINT('Ctrl Pts',(-4.03491384394147,-4.10529399960203,
4.02501255548286));
#60725=CARTESIAN_POINT('Ctrl Pts',(-5.6499911690947,1.10071265112688,3.86801406214079));
#60726=CARTESIAN_POINT('Ctrl Pts',(-2.19876397198699,5.31971855655701,3.71101556879874));
#60727=CARTESIAN_POINT('Ctrl Pts',(3.22407830948427,4.76857290881427,3.55401707545668));
#60728=CARTESIAN_POINT('Ctrl Pts',(5.75591387021709,-0.0585161493539971,
3.39701858211462));
#60729=CARTESIAN_POINT('Ctrl Pts',(3.12646479860794,-4.83313420866293,3.24002008877257));
#60730=CARTESIAN_POINT('Ctrl Pts',(-2.30646165956461,-5.27391724713939,
3.08302159543051));
#60731=CARTESIAN_POINT('Ctrl Pts',(-5.67120141188825,-0.985618387830106,
2.92602310208845));
#60732=CARTESIAN_POINT('Ctrl Pts',(-3.95061740713414,4.18647699637109,2.76902460874639));
#60733=CARTESIAN_POINT('Ctrl Pts',(1.31245513614984,5.60459010746491,2.61202611540434));
#60734=CARTESIAN_POINT('Ctrl Pts',(5.39865967966489,1.99710927213052,2.45502762206228));
#60735=CARTESIAN_POINT('Ctrl Pts',(4.64392553979592,-3.4011639879985,2.29802912872022));
#60736=CARTESIAN_POINT('Ctrl Pts',(-0.274979314205441,-5.74963991794669,
2.14103063537816));
#60737=CARTESIAN_POINT('Ctrl Pts',(-4.94731676851826,-2.94245551640673,
1.9840321420361));
#60738=CARTESIAN_POINT('Ctrl Pts',(-5.18342394835182,2.50320364708249,1.82703364869405));
#60739=CARTESIAN_POINT('Ctrl Pts',(-0.771610415313318,5.70426458692177,
1.67003515535199));
#60740=CARTESIAN_POINT('Ctrl Pts',(4.33213201561917,3.79034363872074,1.51303666200993));
#60741=CARTESIAN_POINT('Ctrl Pts',(5.55122356888078,-1.52232916811941,1.35603816866787));
#60742=CARTESIAN_POINT('Ctrl Pts',(1.79269130257332,-5.46998065428583,1.19903967532582));
#60743=CARTESIAN_POINT('Ctrl Pts',(-3.57355736700018,-4.5126653679007,1.04204118198376));
#60744=CARTESIAN_POINT('Ctrl Pts',(-5.73499497787591,0.490976502422684,
0.885042688641701));
#60745=CARTESIAN_POINT('Ctrl Pts',(-2.75472917190912,5.05464448619777,0.728044195299644));
#60746=CARTESIAN_POINT('Ctrl Pts',(2.6972617242226,5.08531140785296,0.571045701957586));
#60747=CARTESIAN_POINT('Ctrl Pts',(5.72760380327789,0.557054334442611,0.414047208615528));
#60748=CARTESIAN_POINT('Ctrl Pts',(3.62789159583729,-4.47271039022441,0.25704871527347));
#60749=CARTESIAN_POINT('Ctrl Pts',(-1.7363413051643,-5.48787504144657,0.100050221931414));
#60750=CARTESIAN_POINT('Ctrl Pts',(-4.88928570386961,-2.24027593839366,
-0.0307818558536355));
#60751=CARTESIAN_POINT('Ctrl Pts',(-4.96563797731115,1.08580433615736,-0.135447518081672));
#60752=CARTESIAN_POINT('Ctrl Pts',(-4.2377115180993,2.56580265793949,-0.187780349195693));
#60753=CARTESIAN_POINT('Ctrl Pts',(-3.71544298812226,3.17665283523778,-0.213946764752702));
#60754=CARTESIAN_POINT('Ctrl Pts',(-1.21713437249827,-4.54280821229861,
8.21394676475271));
#60755=CARTESIAN_POINT('Ctrl Pts',(-1.96401037376809,-4.34270105156078,
8.1877803491957));
#60756=CARTESIAN_POINT('Ctrl Pts',(-3.34729239311329,-3.56520741493521,
8.13544751808168));
#60757=CARTESIAN_POINT('Ctrl Pts',(-5.097916388523,-0.88550944272982,8.03078185585364));
#60758=CARTESIAN_POINT('Ctrl Pts',(-4.36556770778803,3.40726768821492,7.89994977806859));
#60759=CARTESIAN_POINT('Ctrl Pts',(0.441936745916073,5.52311682288307,7.74295128472654));
#60760=CARTESIAN_POINT('Ctrl Pts',(4.84625712436104,2.6770749043732,7.58595279138447));
#60761=CARTESIAN_POINT('Ctrl Pts',(4.90852145070782,-2.56470983716281,7.42895429804242));
#60762=CARTESIAN_POINT('Ctrl Pts',(0.567509061050049,-5.50921308252134,
7.27195580470035));
#60763=CARTESIAN_POINT('Ctrl Pts',(-4.28142481930937,-3.51235812547142,
7.11495731135831));
#60764=CARTESIAN_POINT('Ctrl Pts',(-5.29173734849243,1.63333062780086,6.95795881801624));
#60765=CARTESIAN_POINT('Ctrl Pts',(-1.55672827609878,5.31477393079903,6.80096032467419));
#60766=CARTESIAN_POINT('Ctrl Pts',(3.57405151254677,4.23031717978746,6.64396183133213));
#60767=CARTESIAN_POINT('Ctrl Pts',(5.50007700619551,-0.647338110797742,
6.48696333799007));
#60768=CARTESIAN_POINT('Ctrl Pts',(2.49418799724395,-4.94457970738323,6.32996484464802));
#60769=CARTESIAN_POINT('Ctrl Pts',(-2.74820137848241,-4.80802812396074,
6.17296635130595));
#60770=CARTESIAN_POINT('Ctrl Pts',(-5.52630929765102,-0.360167388329068,
6.0159678579639));
#60771=CARTESIAN_POINT('Ctrl Pts',(-3.34901207878694,4.41065973951134,5.85896936462184));
#60772=CARTESIAN_POINT('Ctrl Pts',(1.83131632235576,5.22647785209851,5.70197087127978));
#60773=CARTESIAN_POINT('Ctrl Pts',(5.36951859041486,1.35575454917273,5.54497237793772));
#60774=CARTESIAN_POINT('Ctrl Pts',(4.09291324811456,-3.73066463705719,5.38797388459567));
#60775=CARTESIAN_POINT('Ctrl Pts',(-0.853776186777843,-5.47182442937275,
5.23097539125361));
#60776=CARTESIAN_POINT('Ctrl Pts',(-5.03489114715202,-2.30644074453902,
5.07397689791155));
#60777=CARTESIAN_POINT('Ctrl Pts',(-4.70125703915474,2.92711112192079,4.91697840456949));
#60778=CARTESIAN_POINT('Ctrl Pts',(-0.1520412131545,5.53594442208755,4.75997991122743));
#60779=CARTESIAN_POINT('Ctrl Pts',(4.53350885163308,3.18073809941233,4.60298141788538));
#60780=CARTESIAN_POINT('Ctrl Pts',(5.15389566552312,-2.02661213646347,4.44598292454332));
#60781=CARTESIAN_POINT('Ctrl Pts',(1.15282306767785,-5.41671452552386,4.28898443120126));
#60782=CARTESIAN_POINT('Ctrl Pts',(-3.88197729385743,-3.94968980936076,
4.13198593785921));
#60783=CARTESIAN_POINT('Ctrl Pts',(-5.43583785855895,1.05899200924751,3.97498744451714));
#60784=CARTESIAN_POINT('Ctrl Pts',(-2.11542356142786,5.11808366795104,3.81798895117509));
#60785=CARTESIAN_POINT('Ctrl Pts',(3.1018751019502,4.58782825906337,3.66099045783304));
#60786=CARTESIAN_POINT('Ctrl Pts',(5.53774573975908,-0.0562981941875292,
3.50399196449097));
#60787=CARTESIAN_POINT('Ctrl Pts',(3.00796146526509,-4.64994247259256,3.34699347114892));
#60788=CARTESIAN_POINT('Ctrl Pts',(-2.21903915123905,-5.07401837930674,
3.18999497780685));
#60789=CARTESIAN_POINT('Ctrl Pts',(-5.45624416315586,-0.948260198345973,
3.03299648446481));
#60790=CARTESIAN_POINT('Ctrl Pts',(-3.80087597018717,4.0277957026447,2.87599799112274));
#60791=CARTESIAN_POINT('Ctrl Pts',(1.26270875532829,5.39215764699048,2.71899949778069));
#60792=CARTESIAN_POINT('Ctrl Pts',(5.19403266198385,1.92141224016561,2.56200100443863));
#60793=CARTESIAN_POINT('Ctrl Pts',(4.46790543667278,-3.27224864885797,2.40500251109657));
#60794=CARTESIAN_POINT('Ctrl Pts',(-0.264556690752847,-5.53170959098406,
2.24800401775451));
#60795=CARTESIAN_POINT('Ctrl Pts',(-4.75979713662174,-2.83092674209829,
2.09100552441246));
#60796=CARTESIAN_POINT('Ctrl Pts',(-4.9869550751752,2.40832396817252,1.9340070310704));
#60797=CARTESIAN_POINT('Ctrl Pts',(-0.742363834223583,5.48805413474563,
1.77700853772834));
#60798=CARTESIAN_POINT('Ctrl Pts',(4.16792991599511,3.64667710650734,1.62001004438628));
#60799=CARTESIAN_POINT('Ctrl Pts',(5.3408138763307,-1.4646278688924,1.46301155104423));
#60800=CARTESIAN_POINT('Ctrl Pts',(1.7247423862432,-5.26265033630419,1.30601305770217));
#60801=CARTESIAN_POINT('Ctrl Pts',(-3.43810774988952,-4.34162045845692,
1.14901456436011));
#60802=CARTESIAN_POINT('Ctrl Pts',(-5.51761974247093,0.472366872736146,
0.992016071018053));
#60803=CARTESIAN_POINT('Ctrl Pts',(-2.65031584556259,4.86305677961485,0.835017577675994));
#60804=CARTESIAN_POINT('Ctrl Pts',(2.59502660378856,4.89256132373709,0.678019084333937));
#60805=CARTESIAN_POINT('Ctrl Pts',(5.51050871778138,0.535940136862668,0.521020590991879));
#60806=CARTESIAN_POINT('Ctrl Pts',(3.49038253214829,-4.30317990628779,0.364022097649821));
#60807=CARTESIAN_POINT('Ctrl Pts',(-1.67052823969354,-5.27986646713926,
0.207023604307765));
#60808=CARTESIAN_POINT('Ctrl Pts',(-4.70396564082841,-2.15536208731635,
0.0761915265227156));
#60809=CARTESIAN_POINT('Ctrl Pts',(-4.77742391114056,1.04464876861345,-0.0284741357053212));
#60810=CARTESIAN_POINT('Ctrl Pts',(-4.07708826692317,2.46855026993846,-0.0808069668193416));
#60811=CARTESIAN_POINT('Ctrl Pts',(-3.57461543774208,3.05624720968387,-0.106973382376351));
#60812=CARTESIAN_POINT('Ctrl Pts',(-1.16918346556918,-4.3638371975063,8.32092014712906));
#60813=CARTESIAN_POINT('Ctrl Pts',(-1.886635121891,-4.17161357046631,8.29475373157205));
#60814=CARTESIAN_POINT('Ctrl Pts',(-3.21542058862456,-3.4247505082869,8.24242090045803));
#60815=CARTESIAN_POINT('Ctrl Pts',(-4.89707602134433,-0.850623417133479,
8.13775523822999));
#60816=CARTESIAN_POINT('Ctrl Pts',(-4.19357935910711,3.27303306343417,8.00692316044493));
#60817=CARTESIAN_POINT('Ctrl Pts',(0.424525958536476,5.30552502142163,7.84992466710289));
#60818=CARTESIAN_POINT('Ctrl Pts',(4.65533126639873,2.5716073631696,7.69292617376082));
#60819=CARTESIAN_POINT('Ctrl Pts',(4.71514259249745,-2.46366909303406,7.53592768041877));
#60820=CARTESIAN_POINT('Ctrl Pts',(0.545151156464739,-5.29216904059666,
7.3789291870767));
#60821=CARTESIAN_POINT('Ctrl Pts',(-4.11275141095498,-3.37398329900883,
7.22193069373466));
#60822=CARTESIAN_POINT('Ctrl Pts',(-5.08326110229957,1.56898302026649,7.06493220039259));
#60823=CARTESIAN_POINT('Ctrl Pts',(-1.4953985376839,5.10539012251682,6.90793370705054));
#60824=CARTESIAN_POINT('Ctrl Pts',(3.4332461788792,4.06365723660293,6.75093521370847));
#60825=CARTESIAN_POINT('Ctrl Pts',(5.28339289424692,-0.621835216290863,
6.59393672036643));
#60826=CARTESIAN_POINT('Ctrl Pts',(2.3959255709894,-4.74978027791225,6.43693822702436));
#60827=CARTESIAN_POINT('Ctrl Pts',(-2.63993169889764,-4.61860835709371,
6.27993973368231));
#60828=CARTESIAN_POINT('Ctrl Pts',(-5.3085917236669,-0.345978032324596,
6.12294124034025));
#60829=CARTESIAN_POINT('Ctrl Pts',(-3.21707252459896,4.23689491991211,5.96594274699819));
#60830=CARTESIAN_POINT('Ctrl Pts',(1.75916875959262,5.0205726055492,5.80894425365613));
#60831=CARTESIAN_POINT('Ctrl Pts',(5.15797803088363,1.30234248418222,5.65194576031408));
#60832=CARTESIAN_POINT('Ctrl Pts',(3.93166654712268,-3.58368928508518,5.49494726697202));
#60833=CARTESIAN_POINT('Ctrl Pts',(-0.820140342293046,-5.25625337175271,
5.33794877362996));
#60834=CARTESIAN_POINT('Ctrl Pts',(-4.83653375765556,-2.215574914128,5.1809502802879));
#60835=CARTESIAN_POINT('Ctrl Pts',(-4.516043685701,2.81179301395361,5.02395178694585));
#60836=CARTESIAN_POINT('Ctrl Pts',(-0.14605131242859,5.31784725734868,4.86695329360378));
#60837=CARTESIAN_POINT('Ctrl Pts',(4.3549041996581,3.0554279610932,4.70995480026174));
#60838=CARTESIAN_POINT('Ctrl Pts',(4.95084990741799,-1.94677059050708,4.55295630691967));
#60839=CARTESIAN_POINT('Ctrl Pts',(1.1074058049064,-5.20331460851906,4.39595781357761));
#60840=CARTESIAN_POINT('Ctrl Pts',(-3.7290407437734,-3.79408561911948,4.23895932023556));
#60841=CARTESIAN_POINT('Ctrl Pts',(-5.22168454802319,1.01727136736814,4.08196082689349));
#60842=CARTESIAN_POINT('Ctrl Pts',(-2.03208315086874,4.91644877934506,3.92496233355144));
#60843=CARTESIAN_POINT('Ctrl Pts',(2.97967189441612,4.40708360931248,3.76796384020938));
#60844=CARTESIAN_POINT('Ctrl Pts',(5.31957760930108,-0.0540802390210696,
3.61096534686732));
#60845=CARTESIAN_POINT('Ctrl Pts',(2.88945813192224,-4.46675073652217,3.45396685352527));
#60846=CARTESIAN_POINT('Ctrl Pts',(-2.13161664291348,-4.87411951147409,
3.29696836018321));
#60847=CARTESIAN_POINT('Ctrl Pts',(-5.24128691442347,-0.910902008861835,
3.13996986684115));
#60848=CARTESIAN_POINT('Ctrl Pts',(-3.6511345332402,3.86911440891831,2.9829713734991));
#60849=CARTESIAN_POINT('Ctrl Pts',(1.21296237450675,5.17972518651607,2.82597288015703));
#60850=CARTESIAN_POINT('Ctrl Pts',(4.98940564430279,1.8457152082007,2.66897438681498));
#60851=CARTESIAN_POINT('Ctrl Pts',(4.29188533354966,-3.14333330971743,2.51197589347292));
#60852=CARTESIAN_POINT('Ctrl Pts',(-0.254134067300259,-5.31377926402143,
2.35497740013087));
#60853=CARTESIAN_POINT('Ctrl Pts',(-4.57227750472522,-2.71939796778984,
2.1979789067888));
#60854=CARTESIAN_POINT('Ctrl Pts',(-4.79048620199859,2.31344428926255,2.04098041344675));
#60855=CARTESIAN_POINT('Ctrl Pts',(-0.713117253133846,5.27184368256949,
1.88398192010469));
#60856=CARTESIAN_POINT('Ctrl Pts',(4.00372781637104,3.50301057429394,1.72698342676264));
#60857=CARTESIAN_POINT('Ctrl Pts',(5.13040418378061,-1.40692656966539,1.56998493342058));
#60858=CARTESIAN_POINT('Ctrl Pts',(1.65679346991308,-5.05532001832255,1.41298644007852));
#60859=CARTESIAN_POINT('Ctrl Pts',(-3.30265813277885,-4.17057554901314,
1.25598794673646));
#60860=CARTESIAN_POINT('Ctrl Pts',(-5.30024450706594,0.453757243049607,
1.0989894533944));
#60861=CARTESIAN_POINT('Ctrl Pts',(-2.54590251921605,4.67146907303194,0.941990960052346));
#60862=CARTESIAN_POINT('Ctrl Pts',(2.49279148335452,4.69981123962122,0.784992466710289));
#60863=CARTESIAN_POINT('Ctrl Pts',(5.29341363228488,0.514825939282724,0.62799397336823));
#60864=CARTESIAN_POINT('Ctrl Pts',(3.35287346845927,-4.13364942235117,0.470995480026172));
#60865=CARTESIAN_POINT('Ctrl Pts',(-1.60471517422276,-5.07185789283195,
0.313996986684116));
#60866=CARTESIAN_POINT('Ctrl Pts',(-4.51864557778723,-2.07044823623904,
0.183164908899067));
#60867=CARTESIAN_POINT('Ctrl Pts',(-4.58920984496997,1.00349320106954,0.07849924667103));
#60868=CARTESIAN_POINT('Ctrl Pts',(-3.91646501574703,2.37129788193743,0.0261664155570096));
#60869=CARTESIAN_POINT('Ctrl Pts',(-3.43378788736191,2.93584158412995,0.));
#60870=CARTESIAN_POINT('Ctrl Pts',(-3.43378788736191,2.93584158412995,0.));
#60871=CARTESIAN_POINT('Ctrl Pts',(-3.52723777670969,2.83914483717434,2.20957577510153E-16));
#60872=CARTESIAN_POINT('Ctrl Pts',(-3.61593961326928,2.73846171784274,-1.95102593779902E-16));
#60873=CARTESIAN_POINT('Ctrl Pts',(-3.69983889649088,2.63418997519716,-5.55111512312578E-17));
#60874=CARTESIAN_POINT('Ctrl Pts',(-3.78516004991503,2.5281511032253,8.64459958272222E-17));
#60875=CARTESIAN_POINT('Ctrl Pts',(-3.86551489177621,2.41840048478536,3.57207213678775E-15));
#60876=CARTESIAN_POINT('Ctrl Pts',(-3.9408148769991,2.30531248881791,3.33066907387547E-15));
#60877=CARTESIAN_POINT('Ctrl Pts',(-4.01713525064214,2.19069203993958,3.08599476344226E-15));
#60878=CARTESIAN_POINT('Ctrl Pts',(-4.08826327828892,2.07264261686327,1.15541512747695E-15));
#60879=CARTESIAN_POINT('Ctrl Pts',(-4.15406859699169,1.95151684254046,1.38777878078145E-15));
#60880=CARTESIAN_POINT('Ctrl Pts',(-4.21980984783224,1.8305089959106,1.61991620552547E-15));
#60881=CARTESIAN_POINT('Ctrl Pts',(-4.28023911511666,1.70643015108279,2.039107624704E-15));
#60882=CARTESIAN_POINT('Ctrl Pts',(-4.33518267922297,1.57960398874639,2.4980018054066E-15));
#60883=CARTESIAN_POINT('Ctrl Pts',(-4.35306946209471,1.53831594955441,2.64739401730341E-15));
#60884=CARTESIAN_POINT('Ctrl Pts',(-4.37037449182742,1.49673656482301,-1.24977233183131E-15));
#60885=CARTESIAN_POINT('Ctrl Pts',(-4.38709067099901,1.45487653718474,-1.55431223447522E-15));
#60886=CARTESIAN_POINT('Ctrl Pts',(-4.39375920070266,1.43817745572383,-1.67580132393046E-15));
#60887=CARTESIAN_POINT('Ctrl Pts',(-4.40033069663165,1.42144199284245,2.13318250051857E-15));
#60888=CARTESIAN_POINT('Ctrl Pts',(-4.40680423707264,1.40467289792598,2.1094237467878E-15));
#60889=CARTESIAN_POINT('Ctrl Pts',(-4.45933329243635,1.26860134275516,1.91663513266347E-15));
#60890=CARTESIAN_POINT('Ctrl Pts',(-4.50543275765374,1.13027759164836,2.92434253228364E-15));
#60891=CARTESIAN_POINT('Ctrl Pts',(-4.54499128400339,0.990129694249863,
2.63677968348475E-15));
#60892=CARTESIAN_POINT('Ctrl Pts',(-4.58298351161253,0.855530878059325,
2.35904680574097E-15));
#60893=CARTESIAN_POINT('Ctrl Pts',(-4.61494272389214,0.719248781594657,
4.48491542532579E-15));
#60894=CARTESIAN_POINT('Ctrl Pts',(-4.64084676847695,0.58176526830246,3.3584246494911E-15));
#60895=CARTESIAN_POINT('Ctrl Pts',(-4.66691254514768,0.44342337572085,2.22490062051545E-15));
#60896=CARTESIAN_POINT('Ctrl Pts',(-4.68684755285248,0.303864196021266,
1.79312284184644E-16));
#60897=CARTESIAN_POINT('Ctrl Pts',(-4.70058040711193,0.163559265384357,
-6.66133814775094E-16));
#60898=CARTESIAN_POINT('Ctrl Pts',(-4.71271438319262,0.0395896491496948,
-1.41314696648225E-15));
#60899=CARTESIAN_POINT('Ctrl Pts',(-4.72000573130037,-0.0849628385647041,
1.44014651394631E-16));
#60900=CARTESIAN_POINT('Ctrl Pts',(-4.7223714742082,-0.209777558646538,
-3.88578058618805E-16));
#60901=CARTESIAN_POINT('Ctrl Pts',(-4.72292774412613,-0.239125918464476,
-5.13809461450429E-16));
#60902=CARTESIAN_POINT('Ctrl Pts',(-4.72321154151185,-0.268488777105225,
3.0010215925102E-15));
#60903=CARTESIAN_POINT('Ctrl Pts',(-4.72322152198113,-0.297861955465308,
2.91433543964104E-15));
#60904=CARTESIAN_POINT('Ctrl Pts',(-4.72322914092456,-0.320285007726138,
2.84816050575247E-15));
#60905=CARTESIAN_POINT('Ctrl Pts',(-4.72307708136321,-0.342716335801155,
3.67219762837691E-17));
#60906=CARTESIAN_POINT('Ctrl Pts',(-4.72276525050185,-0.365131269043745,
1.38777878078145E-16));
#60907=CARTESIAN_POINT('Ctrl Pts',(-4.72077152616445,-0.508443568958217,
7.91283323787342E-16));
#60908=CARTESIAN_POINT('Ctrl Pts',(-4.71225224775121,-0.651283769357607,
4.69641391259678E-15));
#60909=CARTESIAN_POINT('Ctrl Pts',(-4.69718724960338,-0.793159785562181,
4.52415882534751E-15));
#60910=CARTESIAN_POINT('Ctrl Pts',(-4.68213033873543,-0.934959639059055,
4.35199620907545E-15));
#60911=CARTESIAN_POINT('Ctrl Pts',(-4.66053490666648,-1.07579720961356,
2.29755459169068E-15));
#60912=CARTESIAN_POINT('Ctrl Pts',(-4.63233047059339,-1.21519245994795,
1.88737914186277E-15));
#60913=CARTESIAN_POINT('Ctrl Pts',(-4.62518265294206,-1.25051923720629,
1.78342885146082E-15));
#60914=CARTESIAN_POINT('Ctrl Pts',(-4.61761010448178,-1.28575339934606,
3.86113148383421E-16));
#60915=CARTESIAN_POINT('Ctrl Pts',(-4.60961114292865,-1.32088714489269,
2.22044604925031E-16));
#60916=CARTESIAN_POINT('Ctrl Pts',(-4.57836306126197,-1.45813772958496,
-4.20462921062943E-16));
#60917=CARTESIAN_POINT('Ctrl Pts',(-4.54061164386395,-1.59385666227503,
-3.37562086541692E-16));
#60918=CARTESIAN_POINT('Ctrl Pts',(-4.49667838831439,-1.72776655308613,
-8.04911692853238E-16));
#60919=CARTESIAN_POINT('Ctrl Pts',(-4.46792839524171,-1.81539740094895,
-1.11074602668306E-15));
#60920=CARTESIAN_POINT('Ctrl Pts',(-4.43652997184098,-1.90225339638272,
9.54490265544014E-16));
#60921=CARTESIAN_POINT('Ctrl Pts',(-4.40256174565587,-1.98825353803286,
7.21644966006352E-16));
#60922=CARTESIAN_POINT('Ctrl Pts',(-4.39065014752274,-2.01841110708421,
6.3999337724903E-16));
#60923=CARTESIAN_POINT('Ctrl Pts',(-4.37842246733328,-2.04846340327406,
1.30054899424822E-15));
#60924=CARTESIAN_POINT('Ctrl Pts',(-4.3658818524655,-2.07840682871088,1.27675647831893E-15));
#60925=CARTESIAN_POINT('Ctrl Pts',(-4.35886905063707,-2.09515140709612,
1.26345153267066E-15));
#60926=CARTESIAN_POINT('Ctrl Pts',(-4.35175838797214,-2.11186193915223,
-4.29181623021427E-15));
#60927=CARTESIAN_POINT('Ctrl Pts',(-4.34455039841696,-2.12853778716716,
-4.44089209850063E-15));
#60928=CARTESIAN_POINT('Ctrl Pts',(-4.33665307152192,-2.14680843281913,
-4.60422486348398E-15));
#60929=CARTESIAN_POINT('Ctrl Pts',(-4.3286424353965,-2.16502924396809,5.30168465333661E-15));
#60930=CARTESIAN_POINT('Ctrl Pts',(-4.32052144132994,-2.18319526042712,
5.16253706450698E-15));
#60931=CARTESIAN_POINT('Ctrl Pts',(-4.26272706163057,-2.31247668142725,
4.17227053836974E-15));
#60932=CARTESIAN_POINT('Ctrl Pts',(-4.19931793630604,-2.4390523089761,-3.17224447424671E-16));
#60933=CARTESIAN_POINT('Ctrl Pts',(-4.1306671181063,-2.56266098762457,-5.55111512312578E-17));
#60934=CARTESIAN_POINT('Ctrl Pts',(-4.0593379123478,-2.69109221545352,2.16412797287518E-16));
#60935=CARTESIAN_POINT('Ctrl Pts',(-3.9823498940757,-2.81632115639891,3.16344549884833E-15));
#60936=CARTESIAN_POINT('Ctrl Pts',(-3.90006549167258,-2.93804355166681,
2.74780198594726E-15));
#60937=CARTESIAN_POINT('Ctrl Pts',(-3.81789453604086,-3.05959812639587,
2.33273152715138E-15));
#60938=CARTESIAN_POINT('Ctrl Pts',(-3.73044127702168,-3.17765647132671,
1.52792430062925E-15));
#60939=CARTESIAN_POINT('Ctrl Pts',(-3.63801734753769,-3.29189441139934,
2.04003480774873E-15));
#60940=CARTESIAN_POINT('Ctrl Pts',(-3.56858774848175,-3.37771087062696,
2.42473633883647E-15));
#60941=CARTESIAN_POINT('Ctrl Pts',(-3.49635207705255,-3.46137105631218,
2.6380387160668E-15));
#60942=CARTESIAN_POINT('Ctrl Pts',(-3.42142672585507,-3.54272626619495,
2.95596880306448E-15));
#60943=CARTESIAN_POINT('Ctrl Pts',(-3.38629422705786,-3.58087372586878,
3.10504622773483E-15));
#60944=CARTESIAN_POINT('Ctrl Pts',(-3.3505701767281,-3.61851424013804,2.76570113010457E-15));
#60945=CARTESIAN_POINT('Ctrl Pts',(-3.31426568073248,-3.6556315716941,2.76167977375508E-15));
#60946=CARTESIAN_POINT('Ctrl Pts',(-3.29921135129803,-3.67102295839838,
2.76001224411176E-15));
#60947=CARTESIAN_POINT('Ctrl Pts',(-3.2840555690535,-3.68632600746954,3.617329513469E-16));
#60948=CARTESIAN_POINT('Ctrl Pts',(-3.26880440302003,-3.70153424964867,
5.13478148889135E-16));
#60949=CARTESIAN_POINT('Ctrl Pts',(-3.16314622619418,-3.8068950553632,1.56474995848081E-15));
#60950=CARTESIAN_POINT('Ctrl Pts',(-3.05312027550677,-3.90750387615403,
1.50739186887073E-15));
#60951=CARTESIAN_POINT('Ctrl Pts',(-2.93906465882528,-4.00303742675364,
1.35308431126191E-15));
#60952=CARTESIAN_POINT('Ctrl Pts',(-2.83344548104308,-4.09150457426047,
1.21019053860593E-15));
#60953=CARTESIAN_POINT('Ctrl Pts',(-2.72436990580127,-4.17561968062982,
2.13759783489021E-15));
#60954=CARTESIAN_POINT('Ctrl Pts',(-2.61207533410326,-4.25510133080791,
2.0122792321331E-15));
#60955=CARTESIAN_POINT('Ctrl Pts',(-2.56057702495619,-4.29155162872077,
1.95480810018898E-15));
#60956=CARTESIAN_POINT('Ctrl Pts',(-2.50840133628958,-4.32702707245024,
2.36751160669112E-15));
#60957=CARTESIAN_POINT('Ctrl Pts',(-2.45556938566372,-4.36149843071932,
2.75474087985117E-15));
#60958=CARTESIAN_POINT('Ctrl Pts',(-2.42827777589571,-4.37930543664865,
2.95477343758642E-15));
#60959=CARTESIAN_POINT('Ctrl Pts',(-2.40081102655259,-4.39684448061502,
1.19861602340893E-15));
#60960=CARTESIAN_POINT('Ctrl Pts',(-2.3731719452944,-4.41411137781326,1.24206200879939E-15));
#60961=CARTESIAN_POINT('Ctrl Pts',(-2.35240993886931,-4.42708197648195,
1.27469789200386E-15));
#60962=CARTESIAN_POINT('Ctrl Pts',(-2.3315588675056,-4.43989388919032,-2.42681870829991E-15));
#60963=CARTESIAN_POINT('Ctrl Pts',(-2.310621268056,-4.45254499954709,-2.38004060904018E-15));
#60964=CARTESIAN_POINT('Ctrl Pts',(-2.18359867883944,-4.52929576545271,
-2.09625089852901E-15));
#60965=CARTESIAN_POINT('Ctrl Pts',(-2.0533809663479,-4.60013945799199,1.86447051626453E-17));
#60966=CARTESIAN_POINT('Ctrl Pts',(-1.92026980955225,-4.66473533433833,
-1.2490009027033E-16));
#60967=CARTESIAN_POINT('Ctrl Pts',(-1.7911873441691,-4.72737617657195,-2.64100413770296E-16));
#60968=CARTESIAN_POINT('Ctrl Pts',(-1.65938332691157,-4.78414205363558,
1.04097051092433E-15));
#60969=CARTESIAN_POINT('Ctrl Pts',(-1.52510574125302,-4.83468405991464,
1.71217207078911E-15));
#60970=CARTESIAN_POINT('Ctrl Pts',(-1.45664804130053,-4.8604514989394,2.07094871730909E-15));
#60971=CARTESIAN_POINT('Ctrl Pts',(-1.38754702424773,-4.88460057019718,
-4.86141022577448E-16));
#60972=CARTESIAN_POINT('Ctrl Pts',(-1.31785621200041,-4.90714516622019,
-4.9960036108132E-16));
#60973=CARTESIAN_POINT('Ctrl Pts',(-4.51483246697105,0.00361950456559231,
7.11258330249198));
#60974=CARTESIAN_POINT('Ctrl Pts',(-4.5183463327351,0.455094042321683,7.09669960179219));
#60975=CARTESIAN_POINT('Ctrl Pts',(-4.45593254783999,0.905622974345749,
7.08081590109239));
#60976=CARTESIAN_POINT('Ctrl Pts',(-4.32353239297286,1.33455648409566,7.0649322003926));
#60977=CARTESIAN_POINT('Ctrl Pts',(-3.88730691409435,2.74778538768327,7.01259936927858));
#60978=CARTESIAN_POINT('Ctrl Pts',(-2.69135272588913,3.92658775510004,6.96026653816456));
#60979=CARTESIAN_POINT('Ctrl Pts',(-1.27193484569267,4.34236679115612,6.90793370705054));
#60980=CARTESIAN_POINT('Ctrl Pts',(0.147483034503799,4.75814582721219,6.85560087593652));
#60981=CARTESIAN_POINT('Ctrl Pts',(1.7903646066915,4.41090153190756,6.8032680448225));
#60982=CARTESIAN_POINT('Ctrl Pts',(2.92016317867997,3.45636397543961,6.75093521370848));
#60983=CARTESIAN_POINT('Ctrl Pts',(4.04996175066844,2.50182641897166,6.69860238259446));
#60984=CARTESIAN_POINT('Ctrl Pts',(4.66667732245768,0.939995601340394,6.64626955148044));
#60985=CARTESIAN_POINT('Ctrl Pts',(4.49379055447605,-0.528910651078803,
6.59393672036643));
#60986=CARTESIAN_POINT('Ctrl Pts',(4.32090378649441,-1.997816903498,6.54160388925241));
#60987=CARTESIAN_POINT('Ctrl Pts',(3.35841467874189,-3.37379859070514,6.48927105813838));
#60988=CARTESIAN_POINT('Ctrl Pts',(2.03786057988447,-4.03992744750561,6.43693822702436));
#60989=CARTESIAN_POINT('Ctrl Pts',(0.717306481027035,-4.70605630430607,
6.38460539591034));
#60990=CARTESIAN_POINT('Ctrl Pts',(-0.961312608935302,-4.66233233069989,
6.33227256479632));
#60991=CARTESIAN_POINT('Ctrl Pts',(-2.24539882471135,-3.92836528976861,
6.27993973368231));
#60992=CARTESIAN_POINT('Ctrl Pts',(-3.5294850404874,-3.19439824883733,6.22760690256829));
#60993=CARTESIAN_POINT('Ctrl Pts',(-4.41903838207715,-1.77018814058096,
6.17527407145427));
#60994=CARTESIAN_POINT('Ctrl Pts',(-4.51522851969403,-0.294270927746662,
6.12294124034025));
#60995=CARTESIAN_POINT('Ctrl Pts',(-4.52157464089458,-0.196897644511263,
6.11948859439083));
#60996=CARTESIAN_POINT('Ctrl Pts',(-4.52446751475242,-0.0992992973699645,
6.1160359484414));
#60997=CARTESIAN_POINT('Ctrl Pts',(-4.52399690261043,-0.00167256832429505,
6.11258330249198));
#60998=CARTESIAN_POINT('Ctrl Pts',(-1.31303618635644,-4.90075024188323,
8.));
#60999=CARTESIAN_POINT('Ctrl Pts',(-1.45239709211802,-4.85517655769009,
8.));
#61000=CARTESIAN_POINT('Ctrl Pts',(-1.58927461952972,-4.80351078633936,
8.));
#61001=CARTESIAN_POINT('Ctrl Pts',(-1.72340721958534,-4.74604566824414,
8.));
#61002=CARTESIAN_POINT('Ctrl Pts',(-1.85924970425712,-4.68784800100459,
8.));
#61003=CARTESIAN_POINT('Ctrl Pts',(-1.99227741877149,-4.62370180241543,
8.));
#61004=CARTESIAN_POINT('Ctrl Pts',(-2.1221970609313,-4.55386234778148,8.));
#61005=CARTESIAN_POINT('Ctrl Pts',(-2.25246970806005,-4.48383313219911,
8.));
#61006=CARTESIAN_POINT('Ctrl Pts',(-2.37961793682551,-4.40807921917534,
8.));
#61007=CARTESIAN_POINT('Ctrl Pts',(-2.50331578855033,-4.32681572428032,
8.));
#61008=CARTESIAN_POINT('Ctrl Pts',(-2.62609342189428,-4.24615676827303,
8.));
#61009=CARTESIAN_POINT('Ctrl Pts',(-2.74547232113475,-4.16006940168606,
8.));
#61010=CARTESIAN_POINT('Ctrl Pts',(-2.86109611850811,-4.06872967104376,
8.));
#61011=CARTESIAN_POINT('Ctrl Pts',(-2.9021226048247,-4.0363198359191,8.));
#61012=CARTESIAN_POINT('Ctrl Pts',(-2.94267593191283,-4.00324843420239,
8.));
#61013=CARTESIAN_POINT('Ctrl Pts',(-2.98273884627905,-3.96952246026761,
8.));
#61014=CARTESIAN_POINT('Ctrl Pts',(-2.99980179304064,-3.95515844040447,
8.));
#61015=CARTESIAN_POINT('Ctrl Pts',(-3.01677686159523,-3.94067464141144,
8.));
#61016=CARTESIAN_POINT('Ctrl Pts',(-3.03364692784275,-3.92608549145045,
8.));
#61017=CARTESIAN_POINT('Ctrl Pts',(-3.14433906287484,-3.83035947983968,
8.));
#61018=CARTESIAN_POINT('Ctrl Pts',(-3.25067173076357,-3.72996938710921,
8.));
#61019=CARTESIAN_POINT('Ctrl Pts',(-3.35235942406226,-3.62515267891276,
8.));
#61020=CARTESIAN_POINT('Ctrl Pts',(-3.36192701172294,-3.61529068862227,
8.));
#61021=CARTESIAN_POINT('Ctrl Pts',(-3.37145345441303,-3.60538948288356,
8.));
#61022=CARTESIAN_POINT('Ctrl Pts',(-3.38093849819353,-3.5954492420827,8.));
#61023=CARTESIAN_POINT('Ctrl Pts',(-3.48179697338609,-3.48975046478426,
8.));
#61024=CARTESIAN_POINT('Ctrl Pts',(-3.57797791034191,-3.37964062514819,
8.));
#61025=CARTESIAN_POINT('Ctrl Pts',(-3.6691784190789,-3.26549870852508,8.));
#61026=CARTESIAN_POINT('Ctrl Pts',(-3.75971104108468,-3.1521926849539,8.));
#61027=CARTESIAN_POINT('Ctrl Pts',(-3.84533634314077,-3.03491270174392,
8.));
#61028=CARTESIAN_POINT('Ctrl Pts',(-3.92571335075401,-2.91400477707446,
8.));
#61029=CARTESIAN_POINT('Ctrl Pts',(-3.99657459670685,-2.80741103289235,
8.));
#61030=CARTESIAN_POINT('Ctrl Pts',(-4.06335624155544,-2.69799686623316,
8.));
#61031=CARTESIAN_POINT('Ctrl Pts',(-4.12579142887319,-2.5859898555039,8.));
#61032=CARTESIAN_POINT('Ctrl Pts',(-4.14218052019666,-2.55658827593677,
8.));
#61033=CARTESIAN_POINT('Ctrl Pts',(-4.15826993976141,-2.52700800600865,
8.));
#61034=CARTESIAN_POINT('Ctrl Pts',(-4.17405446883537,-2.49725311040552,
8.));
#61035=CARTESIAN_POINT('Ctrl Pts',(-4.18546373911311,-2.47574587097943,
8.));
#61036=CARTESIAN_POINT('Ctrl Pts',(-4.19671529109329,-2.45414413479639,
8.));
#61037=CARTESIAN_POINT('Ctrl Pts',(-4.20779517261687,-2.4324732839539,8.));
#61038=CARTESIAN_POINT('Ctrl Pts',(-4.27314976421176,-2.30464794545096,
8.));
#61039=CARTESIAN_POINT('Ctrl Pts',(-4.33262109126524,-2.17426237076666,
8.));
#61040=CARTESIAN_POINT('Ctrl Pts',(-4.38592494350939,-2.0416738299269,8.));
#61041=CARTESIAN_POINT('Ctrl Pts',(-4.43841400089354,-1.91111201805743,
8.));
#61042=CARTESIAN_POINT('Ctrl Pts',(-4.48492299905459,-1.7784133775905,8.));
#61043=CARTESIAN_POINT('Ctrl Pts',(-4.52513335521759,-1.64390172617838,
8.));
#61044=CARTESIAN_POINT('Ctrl Pts',(-4.537048107786,-1.60404450537571,8.));
#61045=CARTESIAN_POINT('Ctrl Pts',(-4.54840950403996,-1.5640280227951,8.));
#61046=CARTESIAN_POINT('Ctrl Pts',(-4.55920838150573,-1.52386053965931,
8.));
#61047=CARTESIAN_POINT('Ctrl Pts',(-4.59649237875198,-1.385179057684,8.));
#61048=CARTESIAN_POINT('Ctrl Pts',(-4.62707496138222,-1.24469748534875,
8.));
#61049=CARTESIAN_POINT('Ctrl Pts',(-4.65105491040296,-1.10285889077504,
8.));
#61050=CARTESIAN_POINT('Ctrl Pts',(-4.66554282028716,-1.017164597826,8.));
#61051=CARTESIAN_POINT('Ctrl Pts',(-4.67761961594462,-0.930974942162248,
8.));
#61052=CARTESIAN_POINT('Ctrl Pts',(-4.68729801221865,-0.844388845291519,
8.));
#61053=CARTESIAN_POINT('Ctrl Pts',(-4.69282817886049,-0.794914166739051,
8.));
#61054=CARTESIAN_POINT('Ctrl Pts',(-4.69757516967293,-0.745310079919106,
8.));
#61055=CARTESIAN_POINT('Ctrl Pts',(-4.70154039472519,-0.695595329877529,
8.));
#61056=CARTESIAN_POINT('Ctrl Pts',(-4.70301053775668,-0.677163136906814,
8.));
#61057=CARTESIAN_POINT('Ctrl Pts',(-4.70437287652954,-0.658719449757616,
8.));
#61058=CARTESIAN_POINT('Ctrl Pts',(-4.70562704431493,-0.64027493011297,
8.));
#61059=CARTESIAN_POINT('Ctrl Pts',(-4.71515809633756,-0.500105745165328,
8.));
#61060=CARTESIAN_POINT('Ctrl Pts',(-4.71845973908213,-0.359723770205855,
8.));
#61061=CARTESIAN_POINT('Ctrl Pts',(-4.71568669686701,-0.219543283976319,
8.));
#61062=CARTESIAN_POINT('Ctrl Pts',(-4.71286811953556,-0.0770609450327588,
8.));
#61063=CARTESIAN_POINT('Ctrl Pts',(-4.70377361453064,0.0652140588645918,
8.));
#61064=CARTESIAN_POINT('Ctrl Pts',(-4.68851230252744,0.206844911988138,
8.));
#61065=CARTESIAN_POINT('Ctrl Pts',(-4.67333458060724,0.347700016947462,
8.));
#61066=CARTESIAN_POINT('Ctrl Pts',(-4.65205714501789,0.487918806531984,
8.));
#61067=CARTESIAN_POINT('Ctrl Pts',(-4.62473814484182,0.627057654071025,
8.));
#61068=CARTESIAN_POINT('Ctrl Pts',(-4.605133388788,0.726906958439074,8.));
#61069=CARTESIAN_POINT('Ctrl Pts',(-4.5824162991499,0.826199852698566,8.));
#61070=CARTESIAN_POINT('Ctrl Pts',(-4.55659376741278,0.92476446952987,8.));
#61071=CARTESIAN_POINT('Ctrl Pts',(-4.54451944953447,0.97085214703918,8.));
#61072=CARTESIAN_POINT('Ctrl Pts',(-4.53176599217756,1.01678048248609,8.));
#61073=CARTESIAN_POINT('Ctrl Pts',(-4.5183332282825,1.06253124418397,8.));
#61074=CARTESIAN_POINT('Ctrl Pts',(-4.51267692512135,1.08179609392292,8.));
#61075=CARTESIAN_POINT('Ctrl Pts',(-4.50690016711964,1.10102945232834,8.));
#61076=CARTESIAN_POINT('Ctrl Pts',(-4.50100291315461,1.12022993263941,8.));
#61077=CARTESIAN_POINT('Ctrl Pts',(-4.49471977615854,1.14068678406554,8.));
#61078=CARTESIAN_POINT('Ctrl Pts',(-4.48830254703555,1.16109751332069,8.));
#61079=CARTESIAN_POINT('Ctrl Pts',(-4.48175248385615,1.18145762320509,8.));
#61080=CARTESIAN_POINT('Ctrl Pts',(-4.43884234970562,1.31483878649018,8.));
#61081=CARTESIAN_POINT('Ctrl Pts',(-4.39022235830023,1.4460911608231,8.));
#61082=CARTESIAN_POINT('Ctrl Pts',(-4.33596033524399,1.57478158992507,8.));
#61083=CARTESIAN_POINT('Ctrl Pts',(-4.28905827705606,1.68601677162324,8.));
#61084=CARTESIAN_POINT('Ctrl Pts',(-4.23794008569217,1.79533788193322,8.));
#61085=CARTESIAN_POINT('Ctrl Pts',(-4.18262262022186,1.90244778297798,8.));
#61086=CARTESIAN_POINT('Ctrl Pts',(-4.15876953368252,1.94863395071215,8.));
#61087=CARTESIAN_POINT('Ctrl Pts',(-4.13413534457581,1.9944087336574,8.));
#61088=CARTESIAN_POINT('Ctrl Pts',(-4.10872005342092,2.03974709902823,8.));
#61089=CARTESIAN_POINT('Ctrl Pts',(-4.09757333138634,2.05963174851782,8.));
#61090=CARTESIAN_POINT('Ctrl Pts',(-4.08627634995272,2.07943244040586,8.));
#61091=CARTESIAN_POINT('Ctrl Pts',(-4.0748290615074,2.09914701235749,8.));
#61092=CARTESIAN_POINT('Ctrl Pts',(-4.06286920268517,2.11974433533126,8.));
#61093=CARTESIAN_POINT('Ctrl Pts',(-4.05074975381766,2.1402399100487,8.));
#61094=CARTESIAN_POINT('Ctrl Pts',(-4.0384724823486,2.16062907002492,8.));
#61095=CARTESIAN_POINT('Ctrl Pts',(-3.96920273979072,2.27566699731059,8.));
#61096=CARTESIAN_POINT('Ctrl Pts',(-3.89489711290362,2.38734570786034,8.));
#61097=CARTESIAN_POINT('Ctrl Pts',(-3.81559004701476,2.49525769668179,8.));
#61098=CARTESIAN_POINT('Ctrl Pts',(-3.739663695997,2.59856959519238,8.));
#61099=CARTESIAN_POINT('Ctrl Pts',(-3.65915281331369,2.69842939750744,8.));
#61100=CARTESIAN_POINT('Ctrl Pts',(-3.57405581868196,2.79444797267076,8.));
#61101=CARTESIAN_POINT('Ctrl Pts',(-3.53072763156913,2.8433370175658,8.));
#61102=CARTESIAN_POINT('Ctrl Pts',(-3.48620998149697,2.89122965827726,8.));
#61103=CARTESIAN_POINT('Ctrl Pts',(-3.44054916109509,2.93810681611542,8.));
#61104=CARTESIAN_POINT('Origin',(-1.11022302462516E-15,0.,8.));
#61105=CARTESIAN_POINT('',(4.90747728811182,-8.5,8.));
#61106=CARTESIAN_POINT('',(9.81495457622364,0.,8.));
#61107=CARTESIAN_POINT('',(4.90747728811182,-8.5,8.));
#61108=CARTESIAN_POINT('',(4.90747728811182,8.5,8.));
#61109=CARTESIAN_POINT('',(9.81495457622364,0.,8.));
#61110=CARTESIAN_POINT('',(-4.90747728811182,8.5,8.));
#61111=CARTESIAN_POINT('',(4.90747728811182,8.5,8.));
#61112=CARTESIAN_POINT('',(-9.81495457622364,1.11022302462516E-15,8.));
#61113=CARTESIAN_POINT('',(-4.90747728811182,8.5,8.));
#61114=CARTESIAN_POINT('',(-4.90747728811182,-8.5,8.));
#61115=CARTESIAN_POINT('',(-9.81495457622364,1.20198527055489E-15,8.));
#61116=CARTESIAN_POINT('',(-4.90747728811182,-8.5,8.));
#61117=CARTESIAN_POINT('Origin',(0.,0.,4.));
#61118=CARTESIAN_POINT('Origin',(-4.90747728811182,-8.5,0.));
#61119=CARTESIAN_POINT('',(-4.90747728811182,-8.5,0.));
#61120=CARTESIAN_POINT('',(4.90747728811182,-8.5,0.));
#61121=CARTESIAN_POINT('',(-4.90747728811182,-8.5,0.));
#61122=CARTESIAN_POINT('',(4.90747728811182,-8.5,0.));
#61123=CARTESIAN_POINT('',(-4.90747728811182,-8.5,0.));
#61124=CARTESIAN_POINT('Origin',(-9.81495457622364,1.20198527055489E-15,
0.));
#61125=CARTESIAN_POINT('',(-9.81495457622364,1.20198527055489E-15,0.));
#61126=CARTESIAN_POINT('',(-9.81495457622364,1.20198527055489E-15,0.));
#61127=CARTESIAN_POINT('',(-9.81495457622364,1.20198527055489E-15,0.));
#61128=CARTESIAN_POINT('Origin',(-4.90747728811182,8.5,0.));
#61129=CARTESIAN_POINT('',(-4.90747728811182,8.5,0.));
#61130=CARTESIAN_POINT('',(-4.90747728811182,8.5,0.));
#61131=CARTESIAN_POINT('',(-4.90747728811182,8.5,0.));
#61132=CARTESIAN_POINT('Origin',(4.90747728811182,8.5,0.));
#61133=CARTESIAN_POINT('',(4.90747728811182,8.5,0.));
#61134=CARTESIAN_POINT('',(4.90747728811182,8.5,0.));
#61135=CARTESIAN_POINT('',(4.90747728811182,8.5,0.));
#61136=CARTESIAN_POINT('Origin',(9.81495457622364,0.,0.));
#61137=CARTESIAN_POINT('',(9.81495457622364,0.,0.));
#61138=CARTESIAN_POINT('',(9.81495457622364,0.,0.));
#61139=CARTESIAN_POINT('',(9.81495457622364,0.,0.));
#61140=CARTESIAN_POINT('Origin',(4.90747728811182,-8.5,0.));
#61141=CARTESIAN_POINT('',(4.90747728811182,-8.5,0.));
#61142=CARTESIAN_POINT('Origin',(-1.11022302462516E-15,0.,0.));
#63731=UNCERTAINTY_MEASURE_WITH_UNIT(LENGTH_MEASURE(0.01),#63756,
'DISTANCE_ACCURACY_VALUE',
'Maximum model space distance between geometric entities at asserted c
onnectivities');
#63735=UNCERTAINTY_MEASURE_WITH_UNIT(LENGTH_MEASURE(0.01),#63756,
'DISTANCE_ACCURACY_VALUE',
'Maximum model space distance between geometric entities at asserted c
onnectivities');
#63751=(
GEOMETRIC_REPRESENTATION_CONTEXT(3)
GLOBAL_UNCERTAINTY_ASSIGNED_CONTEXT((#63731))
GLOBAL_UNIT_ASSIGNED_CONTEXT((#63756,#63758,#63759))
REPRESENTATION_CONTEXT('','3D')
);
#63755=(
GEOMETRIC_REPRESENTATION_CONTEXT(3)
GLOBAL_UNCERTAINTY_ASSIGNED_CONTEXT((#63735))
GLOBAL_UNIT_ASSIGNED_CONTEXT((#63756,#63758,#63759))
REPRESENTATION_CONTEXT('','3D')
);
#63756=(
LENGTH_UNIT()
NAMED_UNIT(*)
SI_UNIT(.MILLI.,.METRE.)
);
#63758=(
NAMED_UNIT(*)
PLANE_ANGLE_UNIT()
SI_UNIT($,.RADIAN.)
);
#63759=(
NAMED_UNIT(*)
SI_UNIT($,.STERADIAN.)
SOLID_ANGLE_UNIT()
);
#63775=SHAPE_DEFINITION_REPRESENTATION(#63834,#63873);
#63834=PRODUCT_DEFINITION_SHAPE('',$,#63893);
#63873=SHAPE_REPRESENTATION('',(#15394),#63751);
#63877=PRODUCT_DEFINITION_CONTEXT('part definition',#63936,'design');
#63893=PRODUCT_DEFINITION('Lock nut M10','Lock nut M10',#63912,#63877);
#63912=PRODUCT_DEFINITION_FORMATION('',$,#63953);
#63936=APPLICATION_CONTEXT(
'Core Data for Automotive Mechanical Design Process');
#63937=PRODUCT_CONTEXT('part definition',#63936,'mechanical');
#63953=PRODUCT('Lock nut M10','Lock nut M10',$,(#63937));
#63962=PRESENTATION_STYLE_ASSIGNMENT((#63969));
#63969=SURFACE_STYLE_USAGE(.BOTH.,#63976);
#63976=SURFACE_SIDE_STYLE('',(#63983));
#63983=SURFACE_STYLE_FILL_AREA(#63990);
#63990=FILL_AREA_STYLE('Gray',(#63997));
#63997=FILL_AREA_STYLE_COLOUR('Gray',#64004);
#64004=COLOUR_RGB('Gray',0.407843137254902,0.447058823529412,0.498039215686275);
ENDSEC;
END-ISO-10303-21;
